ISO-10303-21;
HEADER;
/* Generated by software containing ST-Developer
 * from STEP Tools, Inc. (www.steptools.com) 
 */

FILE_DESCRIPTION(
/* description */ (''),
/* implementation_level */ '2;1');

FILE_NAME(
/* name */ 'Base.step',
/* time_stamp */ '2026-10-22T16:03:28+06:00',
/* author */ (''),
/* organization */ (''),
/* preprocessor_version */ 'ST-DEVELOPER v20.2',
/* originating_system */ 'Autodesk Translation Framework v15.15.0.0',
/* authorisation */ '');

FILE_SCHEMA (('AUTOMOTIVE_DESIGN { 1 0 10303 214 3 1 1 }'));
ENDSEC;

DATA;
#10=MECHANICAL_DESIGN_GEOMETRIC_PRESENTATION_REPRESENTATION('',(#84),#6096);
#62=SHAPE_REPRESENTATION_RELATIONSHIP('SRR','None',#6137,#73);
#73=ADVANCED_BREP_SHAPE_REPRESENTATION('',(#95),#6085);
#84=STYLED_ITEM('',(#6234),#95);
#95=MANIFOLD_SOLID_BREP('Base',#3593);
#106=FACE_BOUND('',#517,.T.);
#107=FACE_BOUND('',#522,.T.);
#108=FACE_BOUND('',#524,.T.);
#109=FACE_BOUND('',#529,.T.);
#110=FACE_BOUND('',#535,.T.);
#158=PLANE('',#3734);
#159=PLANE('',#3738);
#160=PLANE('',#3739);
#161=PLANE('',#3743);
#162=PLANE('',#3744);
#163=PLANE('',#3748);
#164=PLANE('',#3749);
#165=PLANE('',#3750);
#166=PLANE('',#3751);
#167=PLANE('',#3752);
#168=PLANE('',#3753);
#169=PLANE('',#3754);
#170=PLANE('',#3755);
#171=PLANE('',#3759);
#172=PLANE('',#3760);
#173=PLANE('',#3764);
#174=PLANE('',#3765);
#175=PLANE('',#3769);
#176=PLANE('',#3770);
#177=PLANE('',#3771);
#178=PLANE('',#3772);
#179=PLANE('',#3773);
#180=PLANE('',#3774);
#181=PLANE('',#3775);
#182=PLANE('',#3776);
#183=PLANE('',#3777);
#184=PLANE('',#3778);
#185=PLANE('',#3779);
#186=PLANE('',#3780);
#187=PLANE('',#3781);
#188=PLANE('',#3782);
#189=PLANE('',#3783);
#190=PLANE('',#3784);
#191=PLANE('',#3785);
#192=PLANE('',#3786);
#193=PLANE('',#3787);
#194=PLANE('',#3788);
#298=FACE_OUTER_BOUND('',#486,.T.);
#299=FACE_OUTER_BOUND('',#487,.T.);
#300=FACE_OUTER_BOUND('',#488,.T.);
#301=FACE_OUTER_BOUND('',#489,.T.);
#302=FACE_OUTER_BOUND('',#490,.T.);
#303=FACE_OUTER_BOUND('',#491,.T.);
#304=FACE_OUTER_BOUND('',#492,.T.);
#305=FACE_OUTER_BOUND('',#493,.T.);
#306=FACE_OUTER_BOUND('',#494,.T.);
#307=FACE_OUTER_BOUND('',#495,.T.);
#308=FACE_OUTER_BOUND('',#496,.T.);
#309=FACE_OUTER_BOUND('',#497,.T.);
#310=FACE_OUTER_BOUND('',#498,.T.);
#311=FACE_OUTER_BOUND('',#499,.T.);
#312=FACE_OUTER_BOUND('',#500,.T.);
#313=FACE_OUTER_BOUND('',#501,.T.);
#314=FACE_OUTER_BOUND('',#502,.T.);
#315=FACE_OUTER_BOUND('',#503,.T.);
#316=FACE_OUTER_BOUND('',#504,.T.);
#317=FACE_OUTER_BOUND('',#505,.T.);
#318=FACE_OUTER_BOUND('',#506,.T.);
#319=FACE_OUTER_BOUND('',#507,.T.);
#320=FACE_OUTER_BOUND('',#508,.T.);
#321=FACE_OUTER_BOUND('',#509,.T.);
#322=FACE_OUTER_BOUND('',#510,.T.);
#323=FACE_OUTER_BOUND('',#511,.T.);
#324=FACE_OUTER_BOUND('',#512,.T.);
#325=FACE_OUTER_BOUND('',#513,.T.);
#326=FACE_OUTER_BOUND('',#514,.T.);
#327=FACE_OUTER_BOUND('',#515,.T.);
#328=FACE_OUTER_BOUND('',#516,.T.);
#329=FACE_OUTER_BOUND('',#518,.T.);
#330=FACE_OUTER_BOUND('',#519,.T.);
#331=FACE_OUTER_BOUND('',#520,.T.);
#332=FACE_OUTER_BOUND('',#521,.T.);
#333=FACE_OUTER_BOUND('',#523,.T.);
#334=FACE_OUTER_BOUND('',#525,.T.);
#335=FACE_OUTER_BOUND('',#526,.T.);
#336=FACE_OUTER_BOUND('',#527,.T.);
#337=FACE_OUTER_BOUND('',#528,.T.);
#338=FACE_OUTER_BOUND('',#530,.T.);
#339=FACE_OUTER_BOUND('',#531,.T.);
#340=FACE_OUTER_BOUND('',#532,.T.);
#341=FACE_OUTER_BOUND('',#533,.T.);
#342=FACE_OUTER_BOUND('',#534,.T.);
#486=EDGE_LOOP('',(#2394,#2395,#2396,#2397));
#487=EDGE_LOOP('',(#2398,#2399,#2400,#2401));
#488=EDGE_LOOP('',(#2402,#2403,#2404,#2405));
#489=EDGE_LOOP('',(#2406,#2407,#2408,#2409));
#490=EDGE_LOOP('',(#2410,#2411,#2412,#2413));
#491=EDGE_LOOP('',(#2414,#2415,#2416,#2417));
#492=EDGE_LOOP('',(#2418,#2419,#2420,#2421));
#493=EDGE_LOOP('',(#2422,#2423,#2424,#2425));
#494=EDGE_LOOP('',(#2426,#2427,#2428,#2429));
#495=EDGE_LOOP('',(#2430,#2431,#2432,#2433));
#496=EDGE_LOOP('',(#2434,#2435,#2436,#2437));
#497=EDGE_LOOP('',(#2438,#2439,#2440,#2441,#2442,#2443,#2444,#2445,#2446,
#2447,#2448,#2449,#2450,#2451,#2452,#2453));
#498=EDGE_LOOP('',(#2454,#2455,#2456,#2457));
#499=EDGE_LOOP('',(#2458,#2459,#2460,#2461));
#500=EDGE_LOOP('',(#2462,#2463,#2464,#2465));
#501=EDGE_LOOP('',(#2466,#2467,#2468,#2469));
#502=EDGE_LOOP('',(#2470,#2471,#2472,#2473));
#503=EDGE_LOOP('',(#2474,#2475,#2476,#2477));
#504=EDGE_LOOP('',(#2478,#2479,#2480,#2481));
#505=EDGE_LOOP('',(#2482,#2483,#2484,#2485));
#506=EDGE_LOOP('',(#2486,#2487,#2488,#2489));
#507=EDGE_LOOP('',(#2490,#2491,#2492,#2493));
#508=EDGE_LOOP('',(#2494,#2495,#2496,#2497));
#509=EDGE_LOOP('',(#2498,#2499,#2500,#2501));
#510=EDGE_LOOP('',(#2502,#2503,#2504,#2505));
#511=EDGE_LOOP('',(#2506,#2507,#2508,#2509));
#512=EDGE_LOOP('',(#2510,#2511,#2512,#2513));
#513=EDGE_LOOP('',(#2514,#2515,#2516,#2517));
#514=EDGE_LOOP('',(#2518,#2519,#2520,#2521));
#515=EDGE_LOOP('',(#2522,#2523,#2524,#2525,#2526,#2527,#2528,#2529,#2530,
#2531,#2532,#2533,#2534,#2535,#2536,#2537,#2538,#2539,#2540,#2541,#2542,
#2543,#2544,#2545,#2546,#2547,#2548,#2549));
#516=EDGE_LOOP('',(#2550,#2551,#2552,#2553));
#517=EDGE_LOOP('',(#2554));
#518=EDGE_LOOP('',(#2555,#2556,#2557,#2558));
#519=EDGE_LOOP('',(#2559,#2560,#2561,#2562));
#520=EDGE_LOOP('',(#2563,#2564,#2565,#2566));
#521=EDGE_LOOP('',(#2567,#2568,#2569,#2570));
#522=EDGE_LOOP('',(#2571));
#523=EDGE_LOOP('',(#2572,#2573,#2574,#2575,#2576,#2577,#2578,#2579,#2580,
#2581,#2582,#2583));
#524=EDGE_LOOP('',(#2584));
#525=EDGE_LOOP('',(#2585,#2586,#2587,#2588));
#526=EDGE_LOOP('',(#2589,#2590,#2591,#2592));
#527=EDGE_LOOP('',(#2593,#2594,#2595,#2596));
#528=EDGE_LOOP('',(#2597,#2598,#2599,#2600));
#529=EDGE_LOOP('',(#2601,#2602,#2603,#2604));
#530=EDGE_LOOP('',(#2605,#2606,#2607,#2608,#2609,#2610,#2611,#2612,#2613,
#2614,#2615,#2616,#2617,#2618,#2619,#2620));
#531=EDGE_LOOP('',(#2621,#2622,#2623,#2624));
#532=EDGE_LOOP('',(#2625,#2626,#2627,#2628));
#533=EDGE_LOOP('',(#2629,#2630,#2631,#2632));
#534=EDGE_LOOP('',(#2633,#2634,#2635,#2636,#2637,#2638,#2639,#2640,#2641,
#2642,#2643,#2644));
#535=EDGE_LOOP('',(#2645));
#726=LINE('',#5062,#1105);
#727=LINE('',#5068,#1106);
#728=LINE('',#5073,#1107);
#729=LINE('',#5075,#1108);
#730=LINE('',#5077,#1109);
#731=LINE('',#5078,#1110);
#732=LINE('',#5084,#1111);
#733=LINE('',#5088,#1112);
#734=LINE('',#5089,#1113);
#735=LINE('',#5090,#1114);
#736=LINE('',#5094,#1115);
#737=LINE('',#5096,#1116);
#738=LINE('',#5098,#1117);
#739=LINE('',#5099,#1118);
#740=LINE('',#5105,#1119);
#741=LINE('',#5109,#1120);
#742=LINE('',#5110,#1121);
#743=LINE('',#5111,#1122);
#744=LINE('',#5115,#1123);
#745=LINE('',#5117,#1124);
#746=LINE('',#5119,#1125);
#747=LINE('',#5120,#1126);
#748=LINE('',#5126,#1127);
#749=LINE('',#5130,#1128);
#750=LINE('',#5131,#1129);
#751=LINE('',#5132,#1130);
#752=LINE('',#5134,#1131);
#753=LINE('',#5135,#1132);
#754=LINE('',#5137,#1133);
#755=LINE('',#5139,#1134);
#756=LINE('',#5141,#1135);
#757=LINE('',#5143,#1136);
#758=LINE('',#5144,#1137);
#759=LINE('',#5147,#1138);
#760=LINE('',#5148,#1139);
#761=LINE('',#5150,#1140);
#762=LINE('',#5152,#1141);
#763=LINE('',#5155,#1142);
#764=LINE('',#5156,#1143);
#765=LINE('',#5160,#1144);
#766=LINE('',#5162,#1145);
#767=LINE('',#5164,#1146);
#768=LINE('',#5165,#1147);
#769=LINE('',#5169,#1148);
#770=LINE('',#5171,#1149);
#771=LINE('',#5173,#1150);
#772=LINE('',#5174,#1151);
#773=LINE('',#5181,#1152);
#774=LINE('',#5183,#1153);
#775=LINE('',#5185,#1154);
#776=LINE('',#5186,#1155);
#777=LINE('',#5190,#1156);
#778=LINE('',#5192,#1157);
#779=LINE('',#5194,#1158);
#780=LINE('',#5195,#1159);
#781=LINE('',#5202,#1160);
#782=LINE('',#5204,#1161);
#783=LINE('',#5206,#1162);
#784=LINE('',#5207,#1163);
#785=LINE('',#5211,#1164);
#786=LINE('',#5213,#1165);
#787=LINE('',#5215,#1166);
#788=LINE('',#5216,#1167);
#789=LINE('',#5222,#1168);
#790=LINE('',#5224,#1169);
#791=LINE('',#5225,#1170);
#792=LINE('',#5227,#1171);
#793=LINE('',#5228,#1172);
#794=LINE('',#5231,#1173);
#795=LINE('',#5233,#1174);
#796=LINE('',#5234,#1175);
#797=LINE('',#5236,#1176);
#798=LINE('',#5237,#1177);
#799=LINE('',#5239,#1178);
#800=LINE('',#5240,#1179);
#801=LINE('',#5244,#1180);
#802=LINE('',#5246,#1181);
#803=LINE('',#5248,#1182);
#804=LINE('',#5249,#1183);
#805=LINE('',#5252,#1184);
#806=LINE('',#5254,#1185);
#807=LINE('',#5255,#1186);
#808=LINE('',#5258,#1187);
#809=LINE('',#5259,#1188);
#810=LINE('',#5262,#1189);
#811=LINE('',#5263,#1190);
#812=LINE('',#5265,#1191);
#813=LINE('',#5269,#1192);
#814=LINE('',#5271,#1193);
#815=LINE('',#5273,#1194);
#816=LINE('',#5274,#1195);
#817=LINE('',#5276,#1196);
#818=LINE('',#5278,#1197);
#819=LINE('',#5280,#1198);
#820=LINE('',#5281,#1199);
#821=LINE('',#5284,#1200);
#822=LINE('',#5285,#1201);
#823=LINE('',#5288,#1202);
#824=LINE('',#5289,#1203);
#825=LINE('',#5292,#1204);
#826=LINE('',#5293,#1205);
#827=LINE('',#5296,#1206);
#828=LINE('',#5297,#1207);
#829=LINE('',#5300,#1208);
#830=LINE('',#5301,#1209);
#831=LINE('',#5304,#1210);
#832=LINE('',#5305,#1211);
#833=LINE('',#5308,#1212);
#834=LINE('',#5309,#1213);
#835=LINE('',#5311,#1214);
#1105=VECTOR('',#4051,11.);
#1106=VECTOR('',#4058,11.);
#1107=VECTOR('',#4063,10.);
#1108=VECTOR('',#4064,10.);
#1109=VECTOR('',#4065,10.);
#1110=VECTOR('',#4066,10.);
#1111=VECTOR('',#4073,10.);
#1112=VECTOR('',#4076,10.);
#1113=VECTOR('',#4077,10.);
#1114=VECTOR('',#4078,10.);
#1115=VECTOR('',#4081,10.);
#1116=VECTOR('',#4082,10.);
#1117=VECTOR('',#4083,10.);
#1118=VECTOR('',#4084,10.);
#1119=VECTOR('',#4091,10.);
#1120=VECTOR('',#4094,10.);
#1121=VECTOR('',#4095,10.);
#1122=VECTOR('',#4096,10.);
#1123=VECTOR('',#4099,10.);
#1124=VECTOR('',#4100,10.);
#1125=VECTOR('',#4101,10.);
#1126=VECTOR('',#4102,10.);
#1127=VECTOR('',#4109,10.);
#1128=VECTOR('',#4112,10.);
#1129=VECTOR('',#4113,10.);
#1130=VECTOR('',#4114,10.);
#1131=VECTOR('',#4117,10.);
#1132=VECTOR('',#4118,10.);
#1133=VECTOR('',#4119,10.);
#1134=VECTOR('',#4120,10.);
#1135=VECTOR('',#4121,10.);
#1136=VECTOR('',#4122,10.);
#1137=VECTOR('',#4123,10.);
#1138=VECTOR('',#4126,10.);
#1139=VECTOR('',#4127,10.);
#1140=VECTOR('',#4130,10.);
#1141=VECTOR('',#4133,10.);
#1142=VECTOR('',#4136,10.);
#1143=VECTOR('',#4137,10.);
#1144=VECTOR('',#4140,10.);
#1145=VECTOR('',#4141,10.);
#1146=VECTOR('',#4142,10.);
#1147=VECTOR('',#4143,10.);
#1148=VECTOR('',#4146,10.);
#1149=VECTOR('',#4147,10.);
#1150=VECTOR('',#4148,10.);
#1151=VECTOR('',#4149,10.);
#1152=VECTOR('',#4158,10.);
#1153=VECTOR('',#4159,10.);
#1154=VECTOR('',#4160,10.);
#1155=VECTOR('',#4161,10.);
#1156=VECTOR('',#4164,10.);
#1157=VECTOR('',#4165,10.);
#1158=VECTOR('',#4166,10.);
#1159=VECTOR('',#4167,10.);
#1160=VECTOR('',#4176,10.);
#1161=VECTOR('',#4177,10.);
#1162=VECTOR('',#4178,10.);
#1163=VECTOR('',#4179,10.);
#1164=VECTOR('',#4182,10.);
#1165=VECTOR('',#4183,10.);
#1166=VECTOR('',#4184,10.);
#1167=VECTOR('',#4185,10.);
#1168=VECTOR('',#4194,10.);
#1169=VECTOR('',#4195,10.);
#1170=VECTOR('',#4196,10.);
#1171=VECTOR('',#4199,10.);
#1172=VECTOR('',#4200,10.);
#1173=VECTOR('',#4203,10.);
#1174=VECTOR('',#4204,10.);
#1175=VECTOR('',#4205,10.);
#1176=VECTOR('',#4208,10.);
#1177=VECTOR('',#4209,10.);
#1178=VECTOR('',#4212,10.);
#1179=VECTOR('',#4213,10.);
#1180=VECTOR('',#4216,10.);
#1181=VECTOR('',#4217,10.);
#1182=VECTOR('',#4218,10.);
#1183=VECTOR('',#4219,10.);
#1184=VECTOR('',#4222,10.);
#1185=VECTOR('',#4223,10.);
#1186=VECTOR('',#4224,10.);
#1187=VECTOR('',#4227,10.);
#1188=VECTOR('',#4228,10.);
#1189=VECTOR('',#4231,10.);
#1190=VECTOR('',#4232,10.);
#1191=VECTOR('',#4235,10.);
#1192=VECTOR('',#4238,10.);
#1193=VECTOR('',#4239,10.);
#1194=VECTOR('',#4240,10.);
#1195=VECTOR('',#4241,10.);
#1196=VECTOR('',#4242,10.);
#1197=VECTOR('',#4243,10.);
#1198=VECTOR('',#4244,10.);
#1199=VECTOR('',#4245,10.);
#1200=VECTOR('',#4248,10.);
#1201=VECTOR('',#4249,10.);
#1202=VECTOR('',#4252,10.);
#1203=VECTOR('',#4253,10.);
#1204=VECTOR('',#4256,10.);
#1205=VECTOR('',#4257,10.);
#1206=VECTOR('',#4260,10.);
#1207=VECTOR('',#4261,10.);
#1208=VECTOR('',#4264,10.);
#1209=VECTOR('',#4265,10.);
#1210=VECTOR('',#4268,10.);
#1211=VECTOR('',#4269,10.);
#1212=VECTOR('',#4272,10.);
#1213=VECTOR('',#4273,10.);
#1214=VECTOR('',#4276,10.);
#1484=CIRCLE('',#3729,11.);
#1485=CIRCLE('',#3730,11.);
#1486=CIRCLE('',#3732,11.);
#1487=CIRCLE('',#3733,11.);
#1488=CIRCLE('',#3736,7.61489399011346);
#1489=CIRCLE('',#3737,7.61489399011346);
#1490=CIRCLE('',#3741,7.61489399011346);
#1491=CIRCLE('',#3742,7.61489399011346);
#1492=CIRCLE('',#3746,7.61489399011346);
#1493=CIRCLE('',#3747,7.61489399011346);
#1494=CIRCLE('',#3757,7.61489399011346);
#1495=CIRCLE('',#3758,7.61489399011346);
#1496=CIRCLE('',#3762,7.61489399011346);
#1497=CIRCLE('',#3763,7.61489399011346);
#1498=CIRCLE('',#3767,7.61489399011346);
#1499=CIRCLE('',#3768,7.61489399011346);
#1590=VERTEX_POINT('',#5059);
#1591=VERTEX_POINT('',#5061);
#1592=VERTEX_POINT('',#5065);
#1593=VERTEX_POINT('',#5067);
#1594=VERTEX_POINT('',#5071);
#1595=VERTEX_POINT('',#5072);
#1596=VERTEX_POINT('',#5074);
#1597=VERTEX_POINT('',#5076);
#1598=VERTEX_POINT('',#5080);
#1599=VERTEX_POINT('',#5082);
#1600=VERTEX_POINT('',#5086);
#1601=VERTEX_POINT('',#5087);
#1602=VERTEX_POINT('',#5092);
#1603=VERTEX_POINT('',#5093);
#1604=VERTEX_POINT('',#5095);
#1605=VERTEX_POINT('',#5097);
#1606=VERTEX_POINT('',#5101);
#1607=VERTEX_POINT('',#5103);
#1608=VERTEX_POINT('',#5107);
#1609=VERTEX_POINT('',#5108);
#1610=VERTEX_POINT('',#5113);
#1611=VERTEX_POINT('',#5114);
#1612=VERTEX_POINT('',#5116);
#1613=VERTEX_POINT('',#5118);
#1614=VERTEX_POINT('',#5122);
#1615=VERTEX_POINT('',#5124);
#1616=VERTEX_POINT('',#5128);
#1617=VERTEX_POINT('',#5129);
#1618=VERTEX_POINT('',#5136);
#1619=VERTEX_POINT('',#5138);
#1620=VERTEX_POINT('',#5140);
#1621=VERTEX_POINT('',#5142);
#1622=VERTEX_POINT('',#5146);
#1623=VERTEX_POINT('',#5154);
#1624=VERTEX_POINT('',#5158);
#1625=VERTEX_POINT('',#5159);
#1626=VERTEX_POINT('',#5161);
#1627=VERTEX_POINT('',#5163);
#1628=VERTEX_POINT('',#5167);
#1629=VERTEX_POINT('',#5168);
#1630=VERTEX_POINT('',#5170);
#1631=VERTEX_POINT('',#5172);
#1632=VERTEX_POINT('',#5179);
#1633=VERTEX_POINT('',#5180);
#1634=VERTEX_POINT('',#5182);
#1635=VERTEX_POINT('',#5184);
#1636=VERTEX_POINT('',#5188);
#1637=VERTEX_POINT('',#5189);
#1638=VERTEX_POINT('',#5191);
#1639=VERTEX_POINT('',#5193);
#1640=VERTEX_POINT('',#5200);
#1641=VERTEX_POINT('',#5201);
#1642=VERTEX_POINT('',#5203);
#1643=VERTEX_POINT('',#5205);
#1644=VERTEX_POINT('',#5209);
#1645=VERTEX_POINT('',#5210);
#1646=VERTEX_POINT('',#5212);
#1647=VERTEX_POINT('',#5214);
#1648=VERTEX_POINT('',#5221);
#1649=VERTEX_POINT('',#5223);
#1650=VERTEX_POINT('',#5230);
#1651=VERTEX_POINT('',#5232);
#1652=VERTEX_POINT('',#5242);
#1653=VERTEX_POINT('',#5243);
#1654=VERTEX_POINT('',#5245);
#1655=VERTEX_POINT('',#5247);
#1656=VERTEX_POINT('',#5251);
#1657=VERTEX_POINT('',#5253);
#1658=VERTEX_POINT('',#5257);
#1659=VERTEX_POINT('',#5261);
#1660=VERTEX_POINT('',#5267);
#1661=VERTEX_POINT('',#5268);
#1662=VERTEX_POINT('',#5270);
#1663=VERTEX_POINT('',#5272);
#1664=VERTEX_POINT('',#5275);
#1665=VERTEX_POINT('',#5277);
#1666=VERTEX_POINT('',#5279);
#1667=VERTEX_POINT('',#5283);
#1668=VERTEX_POINT('',#5287);
#1669=VERTEX_POINT('',#5291);
#1670=VERTEX_POINT('',#5295);
#1671=VERTEX_POINT('',#5299);
#1672=VERTEX_POINT('',#5303);
#1673=VERTEX_POINT('',#5307);
#1909=EDGE_CURVE('',#1590,#1590,#1484,.T.);
#1910=EDGE_CURVE('',#1590,#1591,#726,.T.);
#1911=EDGE_CURVE('',#1591,#1591,#1485,.T.);
#1912=EDGE_CURVE('',#1592,#1592,#1486,.T.);
#1913=EDGE_CURVE('',#1592,#1593,#727,.T.);
#1914=EDGE_CURVE('',#1593,#1593,#1487,.T.);
#1915=EDGE_CURVE('',#1594,#1595,#728,.T.);
#1916=EDGE_CURVE('',#1596,#1594,#729,.T.);
#1917=EDGE_CURVE('',#1596,#1597,#730,.T.);
#1918=EDGE_CURVE('',#1595,#1597,#731,.T.);
#1919=EDGE_CURVE('',#1597,#1598,#1488,.T.);
#1920=EDGE_CURVE('',#1599,#1596,#1489,.T.);
#1921=EDGE_CURVE('',#1599,#1598,#732,.T.);
#1922=EDGE_CURVE('',#1600,#1601,#733,.T.);
#1923=EDGE_CURVE('',#1598,#1600,#734,.T.);
#1924=EDGE_CURVE('',#1601,#1599,#735,.T.);
#1925=EDGE_CURVE('',#1602,#1603,#736,.T.);
#1926=EDGE_CURVE('',#1604,#1602,#737,.T.);
#1927=EDGE_CURVE('',#1604,#1605,#738,.T.);
#1928=EDGE_CURVE('',#1603,#1605,#739,.T.);
#1929=EDGE_CURVE('',#1605,#1606,#1490,.T.);
#1930=EDGE_CURVE('',#1607,#1604,#1491,.T.);
#1931=EDGE_CURVE('',#1607,#1606,#740,.T.);
#1932=EDGE_CURVE('',#1608,#1609,#741,.T.);
#1933=EDGE_CURVE('',#1606,#1608,#742,.T.);
#1934=EDGE_CURVE('',#1609,#1607,#743,.T.);
#1935=EDGE_CURVE('',#1610,#1611,#744,.T.);
#1936=EDGE_CURVE('',#1612,#1610,#745,.T.);
#1937=EDGE_CURVE('',#1612,#1613,#746,.T.);
#1938=EDGE_CURVE('',#1611,#1613,#747,.T.);
#1939=EDGE_CURVE('',#1613,#1614,#1492,.T.);
#1940=EDGE_CURVE('',#1615,#1612,#1493,.T.);
#1941=EDGE_CURVE('',#1615,#1614,#748,.T.);
#1942=EDGE_CURVE('',#1616,#1617,#749,.T.);
#1943=EDGE_CURVE('',#1614,#1616,#750,.T.);
#1944=EDGE_CURVE('',#1617,#1615,#751,.T.);
#1945=EDGE_CURVE('',#1611,#1600,#752,.T.);
#1946=EDGE_CURVE('',#1603,#1616,#753,.T.);
#1947=EDGE_CURVE('',#1618,#1608,#754,.T.);
#1948=EDGE_CURVE('',#1618,#1619,#755,.T.);
#1949=EDGE_CURVE('',#1619,#1620,#756,.T.);
#1950=EDGE_CURVE('',#1621,#1620,#757,.T.);
#1951=EDGE_CURVE('',#1595,#1621,#758,.T.);
#1952=EDGE_CURVE('',#1622,#1609,#759,.T.);
#1953=EDGE_CURVE('',#1622,#1618,#760,.T.);
#1954=EDGE_CURVE('',#1602,#1617,#761,.T.);
#1955=EDGE_CURVE('',#1610,#1601,#762,.T.);
#1956=EDGE_CURVE('',#1623,#1621,#763,.T.);
#1957=EDGE_CURVE('',#1594,#1623,#764,.T.);
#1958=EDGE_CURVE('',#1624,#1625,#765,.T.);
#1959=EDGE_CURVE('',#1626,#1624,#766,.T.);
#1960=EDGE_CURVE('',#1627,#1626,#767,.T.);
#1961=EDGE_CURVE('',#1625,#1627,#768,.T.);
#1962=EDGE_CURVE('',#1628,#1629,#769,.T.);
#1963=EDGE_CURVE('',#1630,#1628,#770,.T.);
#1964=EDGE_CURVE('',#1631,#1630,#771,.T.);
#1965=EDGE_CURVE('',#1631,#1629,#772,.T.);
#1966=EDGE_CURVE('',#1629,#1624,#1494,.T.);
#1967=EDGE_CURVE('',#1626,#1631,#1495,.T.);
#1968=EDGE_CURVE('',#1632,#1633,#773,.T.);
#1969=EDGE_CURVE('',#1634,#1632,#774,.T.);
#1970=EDGE_CURVE('',#1635,#1634,#775,.T.);
#1971=EDGE_CURVE('',#1633,#1635,#776,.T.);
#1972=EDGE_CURVE('',#1636,#1637,#777,.T.);
#1973=EDGE_CURVE('',#1638,#1636,#778,.T.);
#1974=EDGE_CURVE('',#1639,#1638,#779,.T.);
#1975=EDGE_CURVE('',#1639,#1637,#780,.T.);
#1976=EDGE_CURVE('',#1637,#1632,#1496,.T.);
#1977=EDGE_CURVE('',#1634,#1639,#1497,.T.);
#1978=EDGE_CURVE('',#1640,#1641,#781,.T.);
#1979=EDGE_CURVE('',#1642,#1640,#782,.T.);
#1980=EDGE_CURVE('',#1643,#1642,#783,.T.);
#1981=EDGE_CURVE('',#1641,#1643,#784,.T.);
#1982=EDGE_CURVE('',#1644,#1645,#785,.T.);
#1983=EDGE_CURVE('',#1646,#1644,#786,.T.);
#1984=EDGE_CURVE('',#1647,#1646,#787,.T.);
#1985=EDGE_CURVE('',#1647,#1645,#788,.T.);
#1986=EDGE_CURVE('',#1645,#1640,#1498,.T.);
#1987=EDGE_CURVE('',#1642,#1647,#1499,.T.);
#1988=EDGE_CURVE('',#1643,#1648,#789,.T.);
#1989=EDGE_CURVE('',#1649,#1648,#790,.T.);
#1990=EDGE_CURVE('',#1641,#1649,#791,.T.);
#1991=EDGE_CURVE('',#1635,#1646,#792,.T.);
#1992=EDGE_CURVE('',#1633,#1644,#793,.T.);
#1993=EDGE_CURVE('',#1650,#1628,#794,.T.);
#1994=EDGE_CURVE('',#1650,#1651,#795,.T.);
#1995=EDGE_CURVE('',#1651,#1630,#796,.T.);
#1996=EDGE_CURVE('',#1627,#1638,#797,.T.);
#1997=EDGE_CURVE('',#1625,#1636,#798,.T.);
#1998=EDGE_CURVE('',#1648,#1623,#799,.T.);
#1999=EDGE_CURVE('',#1651,#1622,#800,.T.);
#2000=EDGE_CURVE('',#1652,#1653,#801,.T.);
#2001=EDGE_CURVE('',#1654,#1652,#802,.T.);
#2002=EDGE_CURVE('',#1655,#1654,#803,.T.);
#2003=EDGE_CURVE('',#1653,#1655,#804,.T.);
#2004=EDGE_CURVE('',#1656,#1655,#805,.T.);
#2005=EDGE_CURVE('',#1656,#1657,#806,.T.);
#2006=EDGE_CURVE('',#1657,#1653,#807,.T.);
#2007=EDGE_CURVE('',#1658,#1654,#808,.T.);
#2008=EDGE_CURVE('',#1658,#1656,#809,.T.);
#2009=EDGE_CURVE('',#1659,#1652,#810,.T.);
#2010=EDGE_CURVE('',#1659,#1658,#811,.T.);
#2011=EDGE_CURVE('',#1659,#1657,#812,.T.);
#2012=EDGE_CURVE('',#1660,#1661,#813,.T.);
#2013=EDGE_CURVE('',#1662,#1660,#814,.T.);
#2014=EDGE_CURVE('',#1663,#1662,#815,.T.);
#2015=EDGE_CURVE('',#1619,#1663,#816,.T.);
#2016=EDGE_CURVE('',#1664,#1650,#817,.T.);
#2017=EDGE_CURVE('',#1665,#1664,#818,.T.);
#2018=EDGE_CURVE('',#1666,#1665,#819,.T.);
#2019=EDGE_CURVE('',#1661,#1666,#820,.T.);
#2020=EDGE_CURVE('',#1663,#1667,#821,.T.);
#2021=EDGE_CURVE('',#1620,#1667,#822,.T.);
#2022=EDGE_CURVE('',#1662,#1668,#823,.T.);
#2023=EDGE_CURVE('',#1667,#1668,#824,.T.);
#2024=EDGE_CURVE('',#1660,#1669,#825,.T.);
#2025=EDGE_CURVE('',#1668,#1669,#826,.T.);
#2026=EDGE_CURVE('',#1669,#1670,#827,.T.);
#2027=EDGE_CURVE('',#1661,#1670,#828,.T.);
#2028=EDGE_CURVE('',#1671,#1649,#829,.T.);
#2029=EDGE_CURVE('',#1664,#1671,#830,.T.);
#2030=EDGE_CURVE('',#1672,#1671,#831,.T.);
#2031=EDGE_CURVE('',#1665,#1672,#832,.T.);
#2032=EDGE_CURVE('',#1673,#1672,#833,.T.);
#2033=EDGE_CURVE('',#1666,#1673,#834,.T.);
#2034=EDGE_CURVE('',#1670,#1673,#835,.T.);
#2394=ORIENTED_EDGE('',*,*,#1909,.F.);
#2395=ORIENTED_EDGE('',*,*,#1910,.T.);
#2396=ORIENTED_EDGE('',*,*,#1911,.F.);
#2397=ORIENTED_EDGE('',*,*,#1910,.F.);
#2398=ORIENTED_EDGE('',*,*,#1912,.F.);
#2399=ORIENTED_EDGE('',*,*,#1913,.T.);
#2400=ORIENTED_EDGE('',*,*,#1914,.F.);
#2401=ORIENTED_EDGE('',*,*,#1913,.F.);
#2402=ORIENTED_EDGE('',*,*,#1915,.F.);
#2403=ORIENTED_EDGE('',*,*,#1916,.F.);
#2404=ORIENTED_EDGE('',*,*,#1917,.T.);
#2405=ORIENTED_EDGE('',*,*,#1918,.F.);
#2406=ORIENTED_EDGE('',*,*,#1919,.F.);
#2407=ORIENTED_EDGE('',*,*,#1917,.F.);
#2408=ORIENTED_EDGE('',*,*,#1920,.F.);
#2409=ORIENTED_EDGE('',*,*,#1921,.T.);
#2410=ORIENTED_EDGE('',*,*,#1922,.F.);
#2411=ORIENTED_EDGE('',*,*,#1923,.F.);
#2412=ORIENTED_EDGE('',*,*,#1921,.F.);
#2413=ORIENTED_EDGE('',*,*,#1924,.F.);
#2414=ORIENTED_EDGE('',*,*,#1925,.F.);
#2415=ORIENTED_EDGE('',*,*,#1926,.F.);
#2416=ORIENTED_EDGE('',*,*,#1927,.T.);
#2417=ORIENTED_EDGE('',*,*,#1928,.F.);
#2418=ORIENTED_EDGE('',*,*,#1929,.F.);
#2419=ORIENTED_EDGE('',*,*,#1927,.F.);
#2420=ORIENTED_EDGE('',*,*,#1930,.F.);
#2421=ORIENTED_EDGE('',*,*,#1931,.T.);
#2422=ORIENTED_EDGE('',*,*,#1932,.F.);
#2423=ORIENTED_EDGE('',*,*,#1933,.F.);
#2424=ORIENTED_EDGE('',*,*,#1931,.F.);
#2425=ORIENTED_EDGE('',*,*,#1934,.F.);
#2426=ORIENTED_EDGE('',*,*,#1935,.F.);
#2427=ORIENTED_EDGE('',*,*,#1936,.F.);
#2428=ORIENTED_EDGE('',*,*,#1937,.T.);
#2429=ORIENTED_EDGE('',*,*,#1938,.F.);
#2430=ORIENTED_EDGE('',*,*,#1939,.F.);
#2431=ORIENTED_EDGE('',*,*,#1937,.F.);
#2432=ORIENTED_EDGE('',*,*,#1940,.F.);
#2433=ORIENTED_EDGE('',*,*,#1941,.T.);
#2434=ORIENTED_EDGE('',*,*,#1942,.F.);
#2435=ORIENTED_EDGE('',*,*,#1943,.F.);
#2436=ORIENTED_EDGE('',*,*,#1941,.F.);
#2437=ORIENTED_EDGE('',*,*,#1944,.F.);
#2438=ORIENTED_EDGE('',*,*,#1918,.T.);
#2439=ORIENTED_EDGE('',*,*,#1919,.T.);
#2440=ORIENTED_EDGE('',*,*,#1923,.T.);
#2441=ORIENTED_EDGE('',*,*,#1945,.F.);
#2442=ORIENTED_EDGE('',*,*,#1938,.T.);
#2443=ORIENTED_EDGE('',*,*,#1939,.T.);
#2444=ORIENTED_EDGE('',*,*,#1943,.T.);
#2445=ORIENTED_EDGE('',*,*,#1946,.F.);
#2446=ORIENTED_EDGE('',*,*,#1928,.T.);
#2447=ORIENTED_EDGE('',*,*,#1929,.T.);
#2448=ORIENTED_EDGE('',*,*,#1933,.T.);
#2449=ORIENTED_EDGE('',*,*,#1947,.F.);
#2450=ORIENTED_EDGE('',*,*,#1948,.T.);
#2451=ORIENTED_EDGE('',*,*,#1949,.T.);
#2452=ORIENTED_EDGE('',*,*,#1950,.F.);
#2453=ORIENTED_EDGE('',*,*,#1951,.F.);
#2454=ORIENTED_EDGE('',*,*,#1932,.T.);
#2455=ORIENTED_EDGE('',*,*,#1952,.F.);
#2456=ORIENTED_EDGE('',*,*,#1953,.T.);
#2457=ORIENTED_EDGE('',*,*,#1947,.T.);
#2458=ORIENTED_EDGE('',*,*,#1925,.T.);
#2459=ORIENTED_EDGE('',*,*,#1946,.T.);
#2460=ORIENTED_EDGE('',*,*,#1942,.T.);
#2461=ORIENTED_EDGE('',*,*,#1954,.F.);
#2462=ORIENTED_EDGE('',*,*,#1922,.T.);
#2463=ORIENTED_EDGE('',*,*,#1955,.F.);
#2464=ORIENTED_EDGE('',*,*,#1935,.T.);
#2465=ORIENTED_EDGE('',*,*,#1945,.T.);
#2466=ORIENTED_EDGE('',*,*,#1915,.T.);
#2467=ORIENTED_EDGE('',*,*,#1951,.T.);
#2468=ORIENTED_EDGE('',*,*,#1956,.F.);
#2469=ORIENTED_EDGE('',*,*,#1957,.F.);
#2470=ORIENTED_EDGE('',*,*,#1958,.F.);
#2471=ORIENTED_EDGE('',*,*,#1959,.F.);
#2472=ORIENTED_EDGE('',*,*,#1960,.F.);
#2473=ORIENTED_EDGE('',*,*,#1961,.F.);
#2474=ORIENTED_EDGE('',*,*,#1962,.F.);
#2475=ORIENTED_EDGE('',*,*,#1963,.F.);
#2476=ORIENTED_EDGE('',*,*,#1964,.F.);
#2477=ORIENTED_EDGE('',*,*,#1965,.T.);
#2478=ORIENTED_EDGE('',*,*,#1966,.F.);
#2479=ORIENTED_EDGE('',*,*,#1965,.F.);
#2480=ORIENTED_EDGE('',*,*,#1967,.F.);
#2481=ORIENTED_EDGE('',*,*,#1959,.T.);
#2482=ORIENTED_EDGE('',*,*,#1968,.F.);
#2483=ORIENTED_EDGE('',*,*,#1969,.F.);
#2484=ORIENTED_EDGE('',*,*,#1970,.F.);
#2485=ORIENTED_EDGE('',*,*,#1971,.F.);
#2486=ORIENTED_EDGE('',*,*,#1972,.F.);
#2487=ORIENTED_EDGE('',*,*,#1973,.F.);
#2488=ORIENTED_EDGE('',*,*,#1974,.F.);
#2489=ORIENTED_EDGE('',*,*,#1975,.T.);
#2490=ORIENTED_EDGE('',*,*,#1976,.F.);
#2491=ORIENTED_EDGE('',*,*,#1975,.F.);
#2492=ORIENTED_EDGE('',*,*,#1977,.F.);
#2493=ORIENTED_EDGE('',*,*,#1969,.T.);
#2494=ORIENTED_EDGE('',*,*,#1978,.F.);
#2495=ORIENTED_EDGE('',*,*,#1979,.F.);
#2496=ORIENTED_EDGE('',*,*,#1980,.F.);
#2497=ORIENTED_EDGE('',*,*,#1981,.F.);
#2498=ORIENTED_EDGE('',*,*,#1982,.F.);
#2499=ORIENTED_EDGE('',*,*,#1983,.F.);
#2500=ORIENTED_EDGE('',*,*,#1984,.F.);
#2501=ORIENTED_EDGE('',*,*,#1985,.T.);
#2502=ORIENTED_EDGE('',*,*,#1986,.F.);
#2503=ORIENTED_EDGE('',*,*,#1985,.F.);
#2504=ORIENTED_EDGE('',*,*,#1987,.F.);
#2505=ORIENTED_EDGE('',*,*,#1979,.T.);
#2506=ORIENTED_EDGE('',*,*,#1981,.T.);
#2507=ORIENTED_EDGE('',*,*,#1988,.T.);
#2508=ORIENTED_EDGE('',*,*,#1989,.F.);
#2509=ORIENTED_EDGE('',*,*,#1990,.F.);
#2510=ORIENTED_EDGE('',*,*,#1971,.T.);
#2511=ORIENTED_EDGE('',*,*,#1991,.T.);
#2512=ORIENTED_EDGE('',*,*,#1983,.T.);
#2513=ORIENTED_EDGE('',*,*,#1992,.F.);
#2514=ORIENTED_EDGE('',*,*,#1963,.T.);
#2515=ORIENTED_EDGE('',*,*,#1993,.F.);
#2516=ORIENTED_EDGE('',*,*,#1994,.T.);
#2517=ORIENTED_EDGE('',*,*,#1995,.T.);
#2518=ORIENTED_EDGE('',*,*,#1961,.T.);
#2519=ORIENTED_EDGE('',*,*,#1996,.T.);
#2520=ORIENTED_EDGE('',*,*,#1973,.T.);
#2521=ORIENTED_EDGE('',*,*,#1997,.F.);
#2522=ORIENTED_EDGE('',*,*,#1916,.T.);
#2523=ORIENTED_EDGE('',*,*,#1957,.T.);
#2524=ORIENTED_EDGE('',*,*,#1998,.F.);
#2525=ORIENTED_EDGE('',*,*,#1988,.F.);
#2526=ORIENTED_EDGE('',*,*,#1980,.T.);
#2527=ORIENTED_EDGE('',*,*,#1987,.T.);
#2528=ORIENTED_EDGE('',*,*,#1984,.T.);
#2529=ORIENTED_EDGE('',*,*,#1991,.F.);
#2530=ORIENTED_EDGE('',*,*,#1970,.T.);
#2531=ORIENTED_EDGE('',*,*,#1977,.T.);
#2532=ORIENTED_EDGE('',*,*,#1974,.T.);
#2533=ORIENTED_EDGE('',*,*,#1996,.F.);
#2534=ORIENTED_EDGE('',*,*,#1960,.T.);
#2535=ORIENTED_EDGE('',*,*,#1967,.T.);
#2536=ORIENTED_EDGE('',*,*,#1964,.T.);
#2537=ORIENTED_EDGE('',*,*,#1995,.F.);
#2538=ORIENTED_EDGE('',*,*,#1999,.T.);
#2539=ORIENTED_EDGE('',*,*,#1952,.T.);
#2540=ORIENTED_EDGE('',*,*,#1934,.T.);
#2541=ORIENTED_EDGE('',*,*,#1930,.T.);
#2542=ORIENTED_EDGE('',*,*,#1926,.T.);
#2543=ORIENTED_EDGE('',*,*,#1954,.T.);
#2544=ORIENTED_EDGE('',*,*,#1944,.T.);
#2545=ORIENTED_EDGE('',*,*,#1940,.T.);
#2546=ORIENTED_EDGE('',*,*,#1936,.T.);
#2547=ORIENTED_EDGE('',*,*,#1955,.T.);
#2548=ORIENTED_EDGE('',*,*,#1924,.T.);
#2549=ORIENTED_EDGE('',*,*,#1920,.T.);
#2550=ORIENTED_EDGE('',*,*,#2000,.F.);
#2551=ORIENTED_EDGE('',*,*,#2001,.F.);
#2552=ORIENTED_EDGE('',*,*,#2002,.F.);
#2553=ORIENTED_EDGE('',*,*,#2003,.F.);
#2554=ORIENTED_EDGE('',*,*,#1914,.T.);
#2555=ORIENTED_EDGE('',*,*,#2003,.T.);
#2556=ORIENTED_EDGE('',*,*,#2004,.F.);
#2557=ORIENTED_EDGE('',*,*,#2005,.T.);
#2558=ORIENTED_EDGE('',*,*,#2006,.T.);
#2559=ORIENTED_EDGE('',*,*,#2002,.T.);
#2560=ORIENTED_EDGE('',*,*,#2007,.F.);
#2561=ORIENTED_EDGE('',*,*,#2008,.T.);
#2562=ORIENTED_EDGE('',*,*,#2004,.T.);
#2563=ORIENTED_EDGE('',*,*,#2001,.T.);
#2564=ORIENTED_EDGE('',*,*,#2009,.F.);
#2565=ORIENTED_EDGE('',*,*,#2010,.T.);
#2566=ORIENTED_EDGE('',*,*,#2007,.T.);
#2567=ORIENTED_EDGE('',*,*,#2011,.T.);
#2568=ORIENTED_EDGE('',*,*,#2005,.F.);
#2569=ORIENTED_EDGE('',*,*,#2008,.F.);
#2570=ORIENTED_EDGE('',*,*,#2010,.F.);
#2571=ORIENTED_EDGE('',*,*,#1909,.T.);
#2572=ORIENTED_EDGE('',*,*,#2012,.F.);
#2573=ORIENTED_EDGE('',*,*,#2013,.F.);
#2574=ORIENTED_EDGE('',*,*,#2014,.F.);
#2575=ORIENTED_EDGE('',*,*,#2015,.F.);
#2576=ORIENTED_EDGE('',*,*,#1948,.F.);
#2577=ORIENTED_EDGE('',*,*,#1953,.F.);
#2578=ORIENTED_EDGE('',*,*,#1999,.F.);
#2579=ORIENTED_EDGE('',*,*,#1994,.F.);
#2580=ORIENTED_EDGE('',*,*,#2016,.F.);
#2581=ORIENTED_EDGE('',*,*,#2017,.F.);
#2582=ORIENTED_EDGE('',*,*,#2018,.F.);
#2583=ORIENTED_EDGE('',*,*,#2019,.F.);
#2584=ORIENTED_EDGE('',*,*,#1911,.T.);
#2585=ORIENTED_EDGE('',*,*,#2015,.T.);
#2586=ORIENTED_EDGE('',*,*,#2020,.T.);
#2587=ORIENTED_EDGE('',*,*,#2021,.F.);
#2588=ORIENTED_EDGE('',*,*,#1949,.F.);
#2589=ORIENTED_EDGE('',*,*,#2014,.T.);
#2590=ORIENTED_EDGE('',*,*,#2022,.T.);
#2591=ORIENTED_EDGE('',*,*,#2023,.F.);
#2592=ORIENTED_EDGE('',*,*,#2020,.F.);
#2593=ORIENTED_EDGE('',*,*,#2013,.T.);
#2594=ORIENTED_EDGE('',*,*,#2024,.T.);
#2595=ORIENTED_EDGE('',*,*,#2025,.F.);
#2596=ORIENTED_EDGE('',*,*,#2022,.F.);
#2597=ORIENTED_EDGE('',*,*,#2026,.F.);
#2598=ORIENTED_EDGE('',*,*,#2024,.F.);
#2599=ORIENTED_EDGE('',*,*,#2012,.T.);
#2600=ORIENTED_EDGE('',*,*,#2027,.T.);
#2601=ORIENTED_EDGE('',*,*,#2006,.F.);
#2602=ORIENTED_EDGE('',*,*,#2011,.F.);
#2603=ORIENTED_EDGE('',*,*,#2009,.T.);
#2604=ORIENTED_EDGE('',*,*,#2000,.T.);
#2605=ORIENTED_EDGE('',*,*,#1958,.T.);
#2606=ORIENTED_EDGE('',*,*,#1997,.T.);
#2607=ORIENTED_EDGE('',*,*,#1972,.T.);
#2608=ORIENTED_EDGE('',*,*,#1976,.T.);
#2609=ORIENTED_EDGE('',*,*,#1968,.T.);
#2610=ORIENTED_EDGE('',*,*,#1992,.T.);
#2611=ORIENTED_EDGE('',*,*,#1982,.T.);
#2612=ORIENTED_EDGE('',*,*,#1986,.T.);
#2613=ORIENTED_EDGE('',*,*,#1978,.T.);
#2614=ORIENTED_EDGE('',*,*,#1990,.T.);
#2615=ORIENTED_EDGE('',*,*,#2028,.F.);
#2616=ORIENTED_EDGE('',*,*,#2029,.F.);
#2617=ORIENTED_EDGE('',*,*,#2016,.T.);
#2618=ORIENTED_EDGE('',*,*,#1993,.T.);
#2619=ORIENTED_EDGE('',*,*,#1962,.T.);
#2620=ORIENTED_EDGE('',*,*,#1966,.T.);
#2621=ORIENTED_EDGE('',*,*,#2017,.T.);
#2622=ORIENTED_EDGE('',*,*,#2029,.T.);
#2623=ORIENTED_EDGE('',*,*,#2030,.F.);
#2624=ORIENTED_EDGE('',*,*,#2031,.F.);
#2625=ORIENTED_EDGE('',*,*,#2018,.T.);
#2626=ORIENTED_EDGE('',*,*,#2031,.T.);
#2627=ORIENTED_EDGE('',*,*,#2032,.F.);
#2628=ORIENTED_EDGE('',*,*,#2033,.F.);
#2629=ORIENTED_EDGE('',*,*,#2019,.T.);
#2630=ORIENTED_EDGE('',*,*,#2033,.T.);
#2631=ORIENTED_EDGE('',*,*,#2034,.F.);
#2632=ORIENTED_EDGE('',*,*,#2027,.F.);
#2633=ORIENTED_EDGE('',*,*,#2026,.T.);
#2634=ORIENTED_EDGE('',*,*,#2034,.T.);
#2635=ORIENTED_EDGE('',*,*,#2032,.T.);
#2636=ORIENTED_EDGE('',*,*,#2030,.T.);
#2637=ORIENTED_EDGE('',*,*,#2028,.T.);
#2638=ORIENTED_EDGE('',*,*,#1989,.T.);
#2639=ORIENTED_EDGE('',*,*,#1998,.T.);
#2640=ORIENTED_EDGE('',*,*,#1956,.T.);
#2641=ORIENTED_EDGE('',*,*,#1950,.T.);
#2642=ORIENTED_EDGE('',*,*,#2021,.T.);
#2643=ORIENTED_EDGE('',*,*,#2023,.T.);
#2644=ORIENTED_EDGE('',*,*,#2025,.T.);
#2645=ORIENTED_EDGE('',*,*,#1912,.T.);
#3364=CYLINDRICAL_SURFACE('',#3728,11.);
#3365=CYLINDRICAL_SURFACE('',#3731,11.);
#3366=CYLINDRICAL_SURFACE('',#3735,7.61489399011346);
#3367=CYLINDRICAL_SURFACE('',#3740,7.61489399011346);
#3368=CYLINDRICAL_SURFACE('',#3745,7.61489399011346);
#3369=CYLINDRICAL_SURFACE('',#3756,7.61489399011346);
#3370=CYLINDRICAL_SURFACE('',#3761,7.61489399011346);
#3371=CYLINDRICAL_SURFACE('',#3766,7.61489399011346);
#3405=ADVANCED_FACE('',(#298),#3364,.F.);
#3406=ADVANCED_FACE('',(#299),#3365,.F.);
#3407=ADVANCED_FACE('',(#300),#158,.T.);
#3408=ADVANCED_FACE('',(#301),#3366,.F.);
#3409=ADVANCED_FACE('',(#302),#159,.T.);
#3410=ADVANCED_FACE('',(#303),#160,.T.);
#3411=ADVANCED_FACE('',(#304),#3367,.F.);
#3412=ADVANCED_FACE('',(#305),#161,.T.);
#3413=ADVANCED_FACE('',(#306),#162,.T.);
#3414=ADVANCED_FACE('',(#307),#3368,.F.);
#3415=ADVANCED_FACE('',(#308),#163,.T.);
#3416=ADVANCED_FACE('',(#309),#164,.T.);
#3417=ADVANCED_FACE('',(#310),#165,.T.);
#3418=ADVANCED_FACE('',(#311),#166,.T.);
#3419=ADVANCED_FACE('',(#312),#167,.T.);
#3420=ADVANCED_FACE('',(#313),#168,.T.);
#3421=ADVANCED_FACE('',(#314),#169,.F.);
#3422=ADVANCED_FACE('',(#315),#170,.F.);
#3423=ADVANCED_FACE('',(#316),#3369,.F.);
#3424=ADVANCED_FACE('',(#317),#171,.F.);
#3425=ADVANCED_FACE('',(#318),#172,.F.);
#3426=ADVANCED_FACE('',(#319),#3370,.F.);
#3427=ADVANCED_FACE('',(#320),#173,.F.);
#3428=ADVANCED_FACE('',(#321),#174,.F.);
#3429=ADVANCED_FACE('',(#322),#3371,.F.);
#3430=ADVANCED_FACE('',(#323),#175,.T.);
#3431=ADVANCED_FACE('',(#324),#176,.T.);
#3432=ADVANCED_FACE('',(#325),#177,.T.);
#3433=ADVANCED_FACE('',(#326),#178,.T.);
#3434=ADVANCED_FACE('',(#327),#179,.T.);
#3435=ADVANCED_FACE('',(#328,#106),#180,.F.);
#3436=ADVANCED_FACE('',(#329),#181,.T.);
#3437=ADVANCED_FACE('',(#330),#182,.T.);
#3438=ADVANCED_FACE('',(#331),#183,.T.);
#3439=ADVANCED_FACE('',(#332,#107),#184,.T.);
#3440=ADVANCED_FACE('',(#333,#108),#185,.F.);
#3441=ADVANCED_FACE('',(#334),#186,.T.);
#3442=ADVANCED_FACE('',(#335),#187,.T.);
#3443=ADVANCED_FACE('',(#336),#188,.T.);
#3444=ADVANCED_FACE('',(#337,#109),#189,.T.);
#3445=ADVANCED_FACE('',(#338),#190,.T.);
#3446=ADVANCED_FACE('',(#339),#191,.T.);
#3447=ADVANCED_FACE('',(#340),#192,.T.);
#3448=ADVANCED_FACE('',(#341),#193,.T.);
#3449=ADVANCED_FACE('',(#342,#110),#194,.T.);
#3593=CLOSED_SHELL('',(#3405,#3406,#3407,#3408,#3409,#3410,#3411,#3412,
#3413,#3414,#3415,#3416,#3417,#3418,#3419,#3420,#3421,#3422,#3423,#3424,
#3425,#3426,#3427,#3428,#3429,#3430,#3431,#3432,#3433,#3434,#3435,#3436,
#3437,#3438,#3439,#3440,#3441,#3442,#3443,#3444,#3445,#3446,#3447,#3448,
#3449));
#3727=AXIS2_PLACEMENT_3D('',#5057,#4045,#4046);
#3728=AXIS2_PLACEMENT_3D('',#5058,#4047,#4048);
#3729=AXIS2_PLACEMENT_3D('',#5060,#4049,#4050);
#3730=AXIS2_PLACEMENT_3D('',#5063,#4052,#4053);
#3731=AXIS2_PLACEMENT_3D('',#5064,#4054,#4055);
#3732=AXIS2_PLACEMENT_3D('',#5066,#4056,#4057);
#3733=AXIS2_PLACEMENT_3D('',#5069,#4059,#4060);
#3734=AXIS2_PLACEMENT_3D('',#5070,#4061,#4062);
#3735=AXIS2_PLACEMENT_3D('',#5079,#4067,#4068);
#3736=AXIS2_PLACEMENT_3D('',#5081,#4069,#4070);
#3737=AXIS2_PLACEMENT_3D('',#5083,#4071,#4072);
#3738=AXIS2_PLACEMENT_3D('',#5085,#4074,#4075);
#3739=AXIS2_PLACEMENT_3D('',#5091,#4079,#4080);
#3740=AXIS2_PLACEMENT_3D('',#5100,#4085,#4086);
#3741=AXIS2_PLACEMENT_3D('',#5102,#4087,#4088);
#3742=AXIS2_PLACEMENT_3D('',#5104,#4089,#4090);
#3743=AXIS2_PLACEMENT_3D('',#5106,#4092,#4093);
#3744=AXIS2_PLACEMENT_3D('',#5112,#4097,#4098);
#3745=AXIS2_PLACEMENT_3D('',#5121,#4103,#4104);
#3746=AXIS2_PLACEMENT_3D('',#5123,#4105,#4106);
#3747=AXIS2_PLACEMENT_3D('',#5125,#4107,#4108);
#3748=AXIS2_PLACEMENT_3D('',#5127,#4110,#4111);
#3749=AXIS2_PLACEMENT_3D('',#5133,#4115,#4116);
#3750=AXIS2_PLACEMENT_3D('',#5145,#4124,#4125);
#3751=AXIS2_PLACEMENT_3D('',#5149,#4128,#4129);
#3752=AXIS2_PLACEMENT_3D('',#5151,#4131,#4132);
#3753=AXIS2_PLACEMENT_3D('',#5153,#4134,#4135);
#3754=AXIS2_PLACEMENT_3D('',#5157,#4138,#4139);
#3755=AXIS2_PLACEMENT_3D('',#5166,#4144,#4145);
#3756=AXIS2_PLACEMENT_3D('',#5175,#4150,#4151);
#3757=AXIS2_PLACEMENT_3D('',#5176,#4152,#4153);
#3758=AXIS2_PLACEMENT_3D('',#5177,#4154,#4155);
#3759=AXIS2_PLACEMENT_3D('',#5178,#4156,#4157);
#3760=AXIS2_PLACEMENT_3D('',#5187,#4162,#4163);
#3761=AXIS2_PLACEMENT_3D('',#5196,#4168,#4169);
#3762=AXIS2_PLACEMENT_3D('',#5197,#4170,#4171);
#3763=AXIS2_PLACEMENT_3D('',#5198,#4172,#4173);
#3764=AXIS2_PLACEMENT_3D('',#5199,#4174,#4175);
#3765=AXIS2_PLACEMENT_3D('',#5208,#4180,#4181);
#3766=AXIS2_PLACEMENT_3D('',#5217,#4186,#4187);
#3767=AXIS2_PLACEMENT_3D('',#5218,#4188,#4189);
#3768=AXIS2_PLACEMENT_3D('',#5219,#4190,#4191);
#3769=AXIS2_PLACEMENT_3D('',#5220,#4192,#4193);
#3770=AXIS2_PLACEMENT_3D('',#5226,#4197,#4198);
#3771=AXIS2_PLACEMENT_3D('',#5229,#4201,#4202);
#3772=AXIS2_PLACEMENT_3D('',#5235,#4206,#4207);
#3773=AXIS2_PLACEMENT_3D('',#5238,#4210,#4211);
#3774=AXIS2_PLACEMENT_3D('',#5241,#4214,#4215);
#3775=AXIS2_PLACEMENT_3D('',#5250,#4220,#4221);
#3776=AXIS2_PLACEMENT_3D('',#5256,#4225,#4226);
#3777=AXIS2_PLACEMENT_3D('',#5260,#4229,#4230);
#3778=AXIS2_PLACEMENT_3D('',#5264,#4233,#4234);
#3779=AXIS2_PLACEMENT_3D('',#5266,#4236,#4237);
#3780=AXIS2_PLACEMENT_3D('',#5282,#4246,#4247);
#3781=AXIS2_PLACEMENT_3D('',#5286,#4250,#4251);
#3782=AXIS2_PLACEMENT_3D('',#5290,#4254,#4255);
#3783=AXIS2_PLACEMENT_3D('',#5294,#4258,#4259);
#3784=AXIS2_PLACEMENT_3D('',#5298,#4262,#4263);
#3785=AXIS2_PLACEMENT_3D('',#5302,#4266,#4267);
#3786=AXIS2_PLACEMENT_3D('',#5306,#4270,#4271);
#3787=AXIS2_PLACEMENT_3D('',#5310,#4274,#4275);
#3788=AXIS2_PLACEMENT_3D('',#5312,#4277,#4278);
#4045=DIRECTION('axis',(0.,0.,1.));
#4046=DIRECTION('refdir',(1.,0.,0.));
#4047=DIRECTION('center_axis',(0.,-1.,0.));
#4048=DIRECTION('ref_axis',(-1.,0.,0.));
#4049=DIRECTION('center_axis',(0.,-1.,0.));
#4050=DIRECTION('ref_axis',(-1.,0.,0.));
#4051=DIRECTION('',(0.,-1.,0.));
#4052=DIRECTION('center_axis',(0.,1.,0.));
#4053=DIRECTION('ref_axis',(-1.,0.,0.));
#4054=DIRECTION('center_axis',(0.,-1.,0.));
#4055=DIRECTION('ref_axis',(-1.,0.,0.));
#4056=DIRECTION('center_axis',(0.,-1.,0.));
#4057=DIRECTION('ref_axis',(-1.,0.,0.));
#4058=DIRECTION('',(0.,-1.,0.));
#4059=DIRECTION('center_axis',(0.,1.,0.));
#4060=DIRECTION('ref_axis',(-1.,0.,0.));
#4061=DIRECTION('center_axis',(0.,-1.,0.));
#4062=DIRECTION('ref_axis',(1.,0.,0.));
#4063=DIRECTION('',(0.,0.,1.));
#4064=DIRECTION('',(-1.,0.,0.));
#4065=DIRECTION('',(0.,0.,1.));
#4066=DIRECTION('',(1.,0.,0.));
#4067=DIRECTION('center_axis',(0.,0.,-1.));
#4068=DIRECTION('ref_axis',(0.,1.,0.));
#4069=DIRECTION('center_axis',(0.,0.,-1.));
#4070=DIRECTION('ref_axis',(0.,1.,0.));
#4071=DIRECTION('center_axis',(0.,0.,1.));
#4072=DIRECTION('ref_axis',(0.,1.,0.));
#4073=DIRECTION('',(0.,0.,1.));
#4074=DIRECTION('center_axis',(-1.98507404446773E-15,1.,0.));
#4075=DIRECTION('ref_axis',(-1.,-1.98507404446773E-15,0.));
#4076=DIRECTION('',(0.,0.,-1.));
#4077=DIRECTION('',(-1.,-1.98507404446773E-15,0.));
#4078=DIRECTION('',(1.,1.98507404446773E-15,0.));
#4079=DIRECTION('center_axis',(-4.96268511116933E-16,-1.,0.));
#4080=DIRECTION('ref_axis',(1.,-4.96268511116933E-16,0.));
#4081=DIRECTION('',(0.,0.,1.));
#4082=DIRECTION('',(-1.,4.96268511116933E-16,0.));
#4083=DIRECTION('',(0.,0.,1.));
#4084=DIRECTION('',(1.,-4.96268511116933E-16,0.));
#4085=DIRECTION('center_axis',(0.,0.,-1.));
#4086=DIRECTION('ref_axis',(0.,1.,0.));
#4087=DIRECTION('center_axis',(0.,0.,-1.));
#4088=DIRECTION('ref_axis',(0.,1.,0.));
#4089=DIRECTION('center_axis',(0.,0.,1.));
#4090=DIRECTION('ref_axis',(0.,1.,0.));
#4091=DIRECTION('',(0.,0.,1.));
#4092=DIRECTION('center_axis',(-1.4888055333508E-15,1.,0.));
#4093=DIRECTION('ref_axis',(-1.,-1.4888055333508E-15,0.));
#4094=DIRECTION('',(0.,0.,-1.));
#4095=DIRECTION('',(-1.,-1.4888055333508E-15,0.));
#4096=DIRECTION('',(1.,1.4888055333508E-15,0.));
#4097=DIRECTION('center_axis',(-9.92537022233866E-16,-1.,0.));
#4098=DIRECTION('ref_axis',(1.,-9.92537022233866E-16,0.));
#4099=DIRECTION('',(0.,0.,1.));
#4100=DIRECTION('',(-1.,9.92537022233866E-16,0.));
#4101=DIRECTION('',(0.,0.,1.));
#4102=DIRECTION('',(1.,-9.92537022233866E-16,0.));
#4103=DIRECTION('center_axis',(0.,0.,-1.));
#4104=DIRECTION('ref_axis',(0.,1.,0.));
#4105=DIRECTION('center_axis',(0.,0.,-1.));
#4106=DIRECTION('ref_axis',(0.,1.,0.));
#4107=DIRECTION('center_axis',(0.,0.,1.));
#4108=DIRECTION('ref_axis',(0.,1.,0.));
#4109=DIRECTION('',(0.,0.,1.));
#4110=DIRECTION('center_axis',(-1.98507404446773E-15,1.,0.));
#4111=DIRECTION('ref_axis',(-1.,-1.98507404446773E-15,0.));
#4112=DIRECTION('',(0.,0.,-1.));
#4113=DIRECTION('',(-1.,-1.98507404446773E-15,0.));
#4114=DIRECTION('',(1.,1.98507404446773E-15,0.));
#4115=DIRECTION('center_axis',(0.,0.,1.));
#4116=DIRECTION('ref_axis',(1.,0.,0.));
#4117=DIRECTION('',(0.,1.,0.));
#4118=DIRECTION('',(0.,1.,0.));
#4119=DIRECTION('',(0.,1.,0.));
#4120=DIRECTION('',(1.,0.,0.));
#4121=DIRECTION('',(0.,1.,0.));
#4122=DIRECTION('',(1.,0.,0.));
#4123=DIRECTION('',(0.,1.,0.));
#4124=DIRECTION('center_axis',(-1.,0.,0.));
#4125=DIRECTION('ref_axis',(0.,0.,1.));
#4126=DIRECTION('',(0.,1.,0.));
#4127=DIRECTION('',(0.,0.,1.));
#4128=DIRECTION('center_axis',(-1.,0.,0.));
#4129=DIRECTION('ref_axis',(0.,0.,1.));
#4130=DIRECTION('',(0.,1.,0.));
#4131=DIRECTION('center_axis',(-1.,0.,0.));
#4132=DIRECTION('ref_axis',(0.,0.,1.));
#4133=DIRECTION('',(0.,1.,0.));
#4134=DIRECTION('center_axis',(-1.,0.,0.));
#4135=DIRECTION('ref_axis',(0.,0.,1.));
#4136=DIRECTION('',(0.,0.,1.));
#4137=DIRECTION('',(0.,1.,0.));
#4138=DIRECTION('center_axis',(-4.96268511116933E-16,1.,0.));
#4139=DIRECTION('ref_axis',(-1.,-4.96268511116933E-16,0.));
#4140=DIRECTION('',(1.,4.96268511116933E-16,0.));
#4141=DIRECTION('',(0.,0.,1.));
#4142=DIRECTION('',(-1.,-4.96268511116933E-16,0.));
#4143=DIRECTION('',(0.,0.,-1.));
#4144=DIRECTION('center_axis',(-1.4888055333508E-15,-1.,0.));
#4145=DIRECTION('ref_axis',(1.,-1.4888055333508E-15,0.));
#4146=DIRECTION('',(-1.,1.4888055333508E-15,0.));
#4147=DIRECTION('',(0.,0.,1.));
#4148=DIRECTION('',(1.,-1.4888055333508E-15,0.));
#4149=DIRECTION('',(0.,0.,1.));
#4150=DIRECTION('center_axis',(0.,0.,1.));
#4151=DIRECTION('ref_axis',(0.,1.,0.));
#4152=DIRECTION('center_axis',(0.,0.,-1.));
#4153=DIRECTION('ref_axis',(0.,1.,0.));
#4154=DIRECTION('center_axis',(0.,0.,1.));
#4155=DIRECTION('ref_axis',(0.,1.,0.));
#4156=DIRECTION('center_axis',(-9.92537022233866E-16,1.,0.));
#4157=DIRECTION('ref_axis',(-1.,-9.92537022233866E-16,0.));
#4158=DIRECTION('',(1.,9.92537022233866E-16,0.));
#4159=DIRECTION('',(0.,0.,1.));
#4160=DIRECTION('',(-1.,-9.92537022233866E-16,0.));
#4161=DIRECTION('',(0.,0.,-1.));
#4162=DIRECTION('center_axis',(-1.98507404446773E-15,-1.,0.));
#4163=DIRECTION('ref_axis',(1.,-1.98507404446773E-15,0.));
#4164=DIRECTION('',(-1.,1.98507404446773E-15,0.));
#4165=DIRECTION('',(0.,0.,1.));
#4166=DIRECTION('',(1.,-1.98507404446773E-15,0.));
#4167=DIRECTION('',(0.,0.,1.));
#4168=DIRECTION('center_axis',(0.,0.,1.));
#4169=DIRECTION('ref_axis',(0.,1.,0.));
#4170=DIRECTION('center_axis',(0.,0.,-1.));
#4171=DIRECTION('ref_axis',(0.,1.,0.));
#4172=DIRECTION('center_axis',(0.,0.,1.));
#4173=DIRECTION('ref_axis',(0.,1.,0.));
#4174=DIRECTION('center_axis',(0.,1.,0.));
#4175=DIRECTION('ref_axis',(-1.,0.,0.));
#4176=DIRECTION('',(1.,0.,0.));
#4177=DIRECTION('',(0.,0.,1.));
#4178=DIRECTION('',(-1.,0.,0.));
#4179=DIRECTION('',(0.,0.,-1.));
#4180=DIRECTION('center_axis',(-1.98507404446773E-15,-1.,0.));
#4181=DIRECTION('ref_axis',(1.,-1.98507404446773E-15,0.));
#4182=DIRECTION('',(-1.,1.98507404446773E-15,0.));
#4183=DIRECTION('',(0.,0.,1.));
#4184=DIRECTION('',(1.,-1.98507404446773E-15,0.));
#4185=DIRECTION('',(0.,0.,1.));
#4186=DIRECTION('center_axis',(0.,0.,1.));
#4187=DIRECTION('ref_axis',(0.,1.,0.));
#4188=DIRECTION('center_axis',(0.,0.,-1.));
#4189=DIRECTION('ref_axis',(0.,1.,0.));
#4190=DIRECTION('center_axis',(0.,0.,1.));
#4191=DIRECTION('ref_axis',(0.,1.,0.));
#4192=DIRECTION('center_axis',(1.,0.,0.));
#4193=DIRECTION('ref_axis',(0.,0.,-1.));
#4194=DIRECTION('',(0.,1.,0.));
#4195=DIRECTION('',(0.,0.,-1.));
#4196=DIRECTION('',(0.,1.,0.));
#4197=DIRECTION('center_axis',(1.,0.,0.));
#4198=DIRECTION('ref_axis',(0.,0.,-1.));
#4199=DIRECTION('',(0.,1.,0.));
#4200=DIRECTION('',(0.,1.,0.));
#4201=DIRECTION('center_axis',(1.,0.,0.));
#4202=DIRECTION('ref_axis',(0.,0.,-1.));
#4203=DIRECTION('',(0.,1.,0.));
#4204=DIRECTION('',(0.,0.,-1.));
#4205=DIRECTION('',(0.,1.,0.));
#4206=DIRECTION('center_axis',(1.,0.,0.));
#4207=DIRECTION('ref_axis',(0.,0.,-1.));
#4208=DIRECTION('',(0.,1.,0.));
#4209=DIRECTION('',(0.,1.,0.));
#4210=DIRECTION('center_axis',(0.,0.,-1.));
#4211=DIRECTION('ref_axis',(-1.,0.,0.));
#4212=DIRECTION('',(-1.,0.,0.));
#4213=DIRECTION('',(-1.,0.,0.));
#4214=DIRECTION('center_axis',(0.,1.,0.));
#4215=DIRECTION('ref_axis',(0.,0.,1.));
#4216=DIRECTION('',(1.,0.,0.));
#4217=DIRECTION('',(0.,0.,1.));
#4218=DIRECTION('',(-1.,0.,0.));
#4219=DIRECTION('',(0.,0.,-1.));
#4220=DIRECTION('center_axis',(-1.,0.,0.));
#4221=DIRECTION('ref_axis',(0.,0.,1.));
#4222=DIRECTION('',(0.,1.,0.));
#4223=DIRECTION('',(0.,0.,1.));
#4224=DIRECTION('',(0.,1.,0.));
#4225=DIRECTION('center_axis',(0.,0.,1.));
#4226=DIRECTION('ref_axis',(1.,0.,0.));
#4227=DIRECTION('',(0.,1.,0.));
#4228=DIRECTION('',(1.,0.,0.));
#4229=DIRECTION('center_axis',(1.,0.,0.));
#4230=DIRECTION('ref_axis',(0.,0.,-1.));
#4231=DIRECTION('',(0.,1.,0.));
#4232=DIRECTION('',(0.,0.,-1.));
#4233=DIRECTION('center_axis',(0.,1.,0.));
#4234=DIRECTION('ref_axis',(0.,0.,1.));
#4235=DIRECTION('',(1.,0.,0.));
#4236=DIRECTION('center_axis',(0.,1.,0.));
#4237=DIRECTION('ref_axis',(0.,0.,1.));
#4238=DIRECTION('',(1.,0.,0.));
#4239=DIRECTION('',(0.,0.,1.));
#4240=DIRECTION('',(-1.,0.,0.));
#4241=DIRECTION('',(0.,0.,1.));
#4242=DIRECTION('',(1.,0.,0.));
#4243=DIRECTION('',(0.,0.,-1.));
#4244=DIRECTION('',(-1.,0.,0.));
#4245=DIRECTION('',(0.,0.,-1.));
#4246=DIRECTION('center_axis',(-1.,0.,0.));
#4247=DIRECTION('ref_axis',(0.,0.,1.));
#4248=DIRECTION('',(0.,1.,0.));
#4249=DIRECTION('',(0.,0.,1.));
#4250=DIRECTION('center_axis',(0.,0.,-1.));
#4251=DIRECTION('ref_axis',(-1.,0.,0.));
#4252=DIRECTION('',(0.,1.,0.));
#4253=DIRECTION('',(-1.,0.,0.));
#4254=DIRECTION('center_axis',(-1.,0.,0.));
#4255=DIRECTION('ref_axis',(0.,0.,1.));
#4256=DIRECTION('',(0.,1.,0.));
#4257=DIRECTION('',(0.,0.,1.));
#4258=DIRECTION('center_axis',(0.,0.,1.));
#4259=DIRECTION('ref_axis',(1.,0.,0.));
#4260=DIRECTION('',(1.,0.,0.));
#4261=DIRECTION('',(0.,1.,0.));
#4262=DIRECTION('center_axis',(0.,0.,1.));
#4263=DIRECTION('ref_axis',(1.,0.,0.));
#4264=DIRECTION('',(1.,0.,0.));
#4265=DIRECTION('',(0.,1.,0.));
#4266=DIRECTION('center_axis',(1.,0.,0.));
#4267=DIRECTION('ref_axis',(0.,0.,-1.));
#4268=DIRECTION('',(0.,0.,-1.));
#4269=DIRECTION('',(0.,1.,0.));
#4270=DIRECTION('center_axis',(0.,0.,-1.));
#4271=DIRECTION('ref_axis',(-1.,0.,0.));
#4272=DIRECTION('',(-1.,0.,0.));
#4273=DIRECTION('',(0.,1.,0.));
#4274=DIRECTION('center_axis',(1.,0.,0.));
#4275=DIRECTION('ref_axis',(0.,0.,-1.));
#4276=DIRECTION('',(0.,0.,-1.));
#4277=DIRECTION('center_axis',(0.,1.,0.));
#4278=DIRECTION('ref_axis',(0.,0.,1.));
#5057=CARTESIAN_POINT('',(0.,0.,0.));
#5058=CARTESIAN_POINT('Origin',(4.44089209850063E-15,525.425982185852,41.5000000000007));
#5059=CARTESIAN_POINT('',(11.,60.,41.5000000000007));
#5060=CARTESIAN_POINT('Origin',(4.44089209850063E-15,60.,41.5000000000007));
#5061=CARTESIAN_POINT('',(11.,37.,41.5000000000007));
#5062=CARTESIAN_POINT('',(11.,525.425982185852,41.5000000000007));
#5063=CARTESIAN_POINT('Origin',(4.44089209850063E-15,37.,41.5000000000007));
#5064=CARTESIAN_POINT('Origin',(4.44089209850063E-15,525.425982185852,41.5000000000007));
#5065=CARTESIAN_POINT('',(11.,505.5,41.5000000000007));
#5066=CARTESIAN_POINT('Origin',(4.44089209850063E-15,505.5,41.5000000000007));
#5067=CARTESIAN_POINT('',(11.,482.5,41.5000000000007));
#5068=CARTESIAN_POINT('',(11.,525.425982185852,41.5000000000007));
#5069=CARTESIAN_POINT('Origin',(4.44089209850063E-15,482.5,41.5000000000007));
#5070=CARTESIAN_POINT('Origin',(-114.902144094842,473.010523220612,0.));
#5071=CARTESIAN_POINT('',(-89.9999999999987,473.010523220612,1.47437617670221E-12));
#5072=CARTESIAN_POINT('',(-89.9999999999987,473.010523220612,20.0000000000015));
#5073=CARTESIAN_POINT('',(-89.9999999999987,473.010523220612,7.37188088351104E-13));
#5074=CARTESIAN_POINT('',(-79.1078754759798,473.010523220612,0.));
#5075=CARTESIAN_POINT('',(-12.4510720474206,473.010523220612,1.47437617670221E-12));
#5076=CARTESIAN_POINT('',(-79.1078754759798,473.010523220612,20.0000000000015));
#5077=CARTESIAN_POINT('',(-79.1078754759798,473.010523220612,0.));
#5078=CARTESIAN_POINT('',(-102.451072047421,473.010523220612,20.0000000000015));
#5079=CARTESIAN_POINT('Origin',(-79.1078754759798,465.395629230499,0.));
#5080=CARTESIAN_POINT('',(-79.1078754759798,457.780735240385,20.0000000000015));
#5081=CARTESIAN_POINT('Origin',(-79.1078754759798,465.395629230499,20.0000000000015));
#5082=CARTESIAN_POINT('',(-79.1078754759798,457.780735240385,0.));
#5083=CARTESIAN_POINT('Origin',(-79.1078754759798,465.395629230499,1.47437617670221E-12));
#5084=CARTESIAN_POINT('',(-79.1078754759798,457.780735240385,0.));
#5085=CARTESIAN_POINT('Origin',(-79.1078754759798,457.780735240385,0.));
#5086=CARTESIAN_POINT('',(-89.9999999999987,457.780735240385,20.0000000000015));
#5087=CARTESIAN_POINT('',(-89.9999999999987,457.780735240385,1.47437617670221E-12));
#5088=CARTESIAN_POINT('',(-89.9999999999987,457.780735240385,7.37188088351104E-13));
#5089=CARTESIAN_POINT('',(-84.5539377379897,457.780735240385,20.0000000000015));
#5090=CARTESIAN_POINT('',(5.44606226201027,457.780735240385,1.47437617670221E-12));
#5091=CARTESIAN_POINT('Origin',(-114.902144094842,85.0105232206121,0.));
#5092=CARTESIAN_POINT('',(-89.9999999999987,85.0105232206121,1.47437617670221E-12));
#5093=CARTESIAN_POINT('',(-89.9999999999987,85.0105232206121,20.0000000000015));
#5094=CARTESIAN_POINT('',(-89.9999999999987,85.0105232206121,7.37188088351104E-13));
#5095=CARTESIAN_POINT('',(-79.1078754759798,85.0105232206121,0.));
#5096=CARTESIAN_POINT('',(-12.4510720474206,85.0105232206121,1.47437617670221E-12));
#5097=CARTESIAN_POINT('',(-79.1078754759798,85.0105232206121,20.0000000000015));
#5098=CARTESIAN_POINT('',(-79.1078754759798,85.0105232206121,0.));
#5099=CARTESIAN_POINT('',(-102.451072047421,85.0105232206121,20.0000000000015));
#5100=CARTESIAN_POINT('Origin',(-79.1078754759798,77.3956292304987,0.));
#5101=CARTESIAN_POINT('',(-79.1078754759798,69.7807352403852,20.0000000000015));
#5102=CARTESIAN_POINT('Origin',(-79.1078754759798,77.3956292304987,20.0000000000015));
#5103=CARTESIAN_POINT('',(-79.1078754759798,69.7807352403852,0.));
#5104=CARTESIAN_POINT('Origin',(-79.1078754759798,77.3956292304987,1.47437617670221E-12));
#5105=CARTESIAN_POINT('',(-79.1078754759798,69.7807352403852,0.));
#5106=CARTESIAN_POINT('Origin',(-79.1078754759798,69.7807352403852,0.));
#5107=CARTESIAN_POINT('',(-89.9999999999987,69.7807352403852,20.0000000000015));
#5108=CARTESIAN_POINT('',(-89.9999999999987,69.7807352403852,1.47437617670221E-12));
#5109=CARTESIAN_POINT('',(-89.9999999999987,69.7807352403852,7.37188088351104E-13));
#5110=CARTESIAN_POINT('',(-84.5539377379893,69.7807352403852,20.0000000000015));
#5111=CARTESIAN_POINT('',(5.44606226201067,69.7807352403853,1.47437617670221E-12));
#5112=CARTESIAN_POINT('Origin',(-114.902144094842,299.010523220612,0.));
#5113=CARTESIAN_POINT('',(-89.9999999999987,299.010523220612,1.47437617670221E-12));
#5114=CARTESIAN_POINT('',(-89.9999999999987,299.010523220612,20.0000000000015));
#5115=CARTESIAN_POINT('',(-89.9999999999987,299.010523220612,7.37188088351104E-13));
#5116=CARTESIAN_POINT('',(-79.1078754759798,299.010523220612,0.));
#5117=CARTESIAN_POINT('',(-12.4510720474204,299.010523220612,1.47437617670221E-12));
#5118=CARTESIAN_POINT('',(-79.1078754759798,299.010523220612,20.0000000000015));
#5119=CARTESIAN_POINT('',(-79.1078754759798,299.010523220612,0.));
#5120=CARTESIAN_POINT('',(-102.45107204742,299.010523220612,20.0000000000015));
#5121=CARTESIAN_POINT('Origin',(-79.1078754759798,291.395629230499,0.));
#5122=CARTESIAN_POINT('',(-79.1078754759798,283.780735240385,20.0000000000015));
#5123=CARTESIAN_POINT('Origin',(-79.1078754759798,291.395629230499,20.0000000000015));
#5124=CARTESIAN_POINT('',(-79.1078754759798,283.780735240385,0.));
#5125=CARTESIAN_POINT('Origin',(-79.1078754759798,291.395629230499,1.47437617670221E-12));
#5126=CARTESIAN_POINT('',(-79.1078754759798,283.780735240385,0.));
#5127=CARTESIAN_POINT('Origin',(-79.1078754759798,283.780735240385,0.));
#5128=CARTESIAN_POINT('',(-89.9999999999987,283.780735240385,20.0000000000015));
#5129=CARTESIAN_POINT('',(-89.9999999999987,283.780735240385,1.47437617670221E-12));
#5130=CARTESIAN_POINT('',(-89.9999999999987,283.780735240385,7.37188088351104E-13));
#5131=CARTESIAN_POINT('',(-84.5539377379896,283.780735240385,20.0000000000015));
#5132=CARTESIAN_POINT('',(5.44606226201044,283.780735240385,1.47437617670221E-12));
#5133=CARTESIAN_POINT('Origin',(-89.9999999999987,0.,20.0000000000015));
#5134=CARTESIAN_POINT('',(-89.9999999999987,0.,20.0000000000015));
#5135=CARTESIAN_POINT('',(-89.9999999999987,0.,20.0000000000015));
#5136=CARTESIAN_POINT('',(-89.9999999999987,37.,20.0000000000015));
#5137=CARTESIAN_POINT('',(-89.9999999999987,0.,20.0000000000015));
#5138=CARTESIAN_POINT('',(-51.5061608111161,37.,20.0000000000015));
#5139=CARTESIAN_POINT('',(-44.9999999999988,37.,20.0000000000015));
#5140=CARTESIAN_POINT('',(-51.5061608111161,505.5,20.0000000000015));
#5141=CARTESIAN_POINT('',(-51.5061608111161,0.,20.0000000000015));
#5142=CARTESIAN_POINT('',(-89.9999999999987,505.5,20.0000000000015));
#5143=CARTESIAN_POINT('',(90.0000000000013,505.5,20.0000000000015));
#5144=CARTESIAN_POINT('',(-89.9999999999987,0.,20.0000000000015));
#5145=CARTESIAN_POINT('Origin',(-89.9999999999987,0.,1.47437617670221E-12));
#5146=CARTESIAN_POINT('',(-89.9999999999987,37.,1.47437617670221E-12));
#5147=CARTESIAN_POINT('',(-89.9999999999987,0.,1.47437617670221E-12));
#5148=CARTESIAN_POINT('',(-89.9999999999987,37.,26.2500000000015));
#5149=CARTESIAN_POINT('Origin',(-89.9999999999987,0.,1.47437617670221E-12));
#5150=CARTESIAN_POINT('',(-89.9999999999987,0.,1.47437617670221E-12));
#5151=CARTESIAN_POINT('Origin',(-89.9999999999987,0.,1.47437617670221E-12));
#5152=CARTESIAN_POINT('',(-89.9999999999987,0.,1.47437617670221E-12));
#5153=CARTESIAN_POINT('Origin',(-89.9999999999987,0.,1.47437617670221E-12));
#5154=CARTESIAN_POINT('',(-89.9999999999987,505.5,1.47437617670221E-12));
#5155=CARTESIAN_POINT('',(-89.9999999999987,505.5,20.0000000000015));
#5156=CARTESIAN_POINT('',(-89.9999999999987,0.,1.47437617670221E-12));
#5157=CARTESIAN_POINT('Origin',(114.902144094842,85.0105232206121,0.));
#5158=CARTESIAN_POINT('',(79.1078754759798,85.0105232206121,20.0000000000015));
#5159=CARTESIAN_POINT('',(90.0000000000013,85.0105232206121,20.0000000000015));
#5160=CARTESIAN_POINT('',(83.2041524529792,85.0105232206121,20.0000000000015));
#5161=CARTESIAN_POINT('',(79.1078754759798,85.0105232206121,0.));
#5162=CARTESIAN_POINT('',(79.1078754759798,85.0105232206121,0.));
#5163=CARTESIAN_POINT('',(90.0000000000013,85.0105232206121,1.47437617670221E-12));
#5164=CARTESIAN_POINT('',(102.451072047422,85.0105232206121,1.47437617670221E-12));
#5165=CARTESIAN_POINT('',(90.0000000000013,85.0105232206121,10.0000000000007));
#5166=CARTESIAN_POINT('Origin',(79.1078754759798,69.7807352403852,0.));
#5167=CARTESIAN_POINT('',(90.0000000000013,69.7807352403852,20.0000000000015));
#5168=CARTESIAN_POINT('',(79.1078754759798,69.7807352403852,20.0000000000015));
#5169=CARTESIAN_POINT('',(65.307018143548,69.7807352403852,20.0000000000015));
#5170=CARTESIAN_POINT('',(90.0000000000013,69.7807352403852,1.47437617670221E-12));
#5171=CARTESIAN_POINT('',(90.0000000000013,69.7807352403852,10.0000000000007));
#5172=CARTESIAN_POINT('',(79.1078754759798,69.7807352403852,0.));
#5173=CARTESIAN_POINT('',(84.5539377379906,69.7807352403852,1.47437617670221E-12));
#5174=CARTESIAN_POINT('',(79.1078754759798,69.7807352403852,0.));
#5175=CARTESIAN_POINT('Origin',(79.1078754759798,77.3956292304987,0.));
#5176=CARTESIAN_POINT('Origin',(79.1078754759798,77.3956292304987,20.0000000000015));
#5177=CARTESIAN_POINT('Origin',(79.1078754759798,77.3956292304987,1.47437617670221E-12));
#5178=CARTESIAN_POINT('Origin',(114.902144094842,299.010523220612,0.));
#5179=CARTESIAN_POINT('',(79.1078754759798,299.010523220612,20.0000000000015));
#5180=CARTESIAN_POINT('',(90.0000000000013,299.010523220612,20.0000000000015));
#5181=CARTESIAN_POINT('',(83.2041524529791,299.010523220612,20.0000000000015));
#5182=CARTESIAN_POINT('',(79.1078754759798,299.010523220612,0.));
#5183=CARTESIAN_POINT('',(79.1078754759798,299.010523220612,0.));
#5184=CARTESIAN_POINT('',(90.0000000000013,299.010523220612,1.47437617670221E-12));
#5185=CARTESIAN_POINT('',(102.451072047422,299.010523220612,1.47437617670221E-12));
#5186=CARTESIAN_POINT('',(90.0000000000013,299.010523220612,10.0000000000007));
#5187=CARTESIAN_POINT('Origin',(79.1078754759798,283.780735240385,0.));
#5188=CARTESIAN_POINT('',(90.0000000000013,283.780735240385,20.0000000000015));
#5189=CARTESIAN_POINT('',(79.1078754759798,283.780735240385,20.0000000000015));
#5190=CARTESIAN_POINT('',(65.3070181435482,283.780735240385,20.0000000000015));
#5191=CARTESIAN_POINT('',(90.0000000000013,283.780735240385,1.47437617670221E-12));
#5192=CARTESIAN_POINT('',(90.0000000000013,283.780735240385,10.0000000000007));
#5193=CARTESIAN_POINT('',(79.1078754759798,283.780735240385,0.));
#5194=CARTESIAN_POINT('',(84.5539377379908,283.780735240385,1.47437617670221E-12));
#5195=CARTESIAN_POINT('',(79.1078754759798,283.780735240385,0.));
#5196=CARTESIAN_POINT('Origin',(79.1078754759798,291.395629230499,0.));
#5197=CARTESIAN_POINT('Origin',(79.1078754759798,291.395629230499,20.0000000000015));
#5198=CARTESIAN_POINT('Origin',(79.1078754759798,291.395629230499,1.47437617670221E-12));
#5199=CARTESIAN_POINT('Origin',(114.902144094842,473.010523220612,0.));
#5200=CARTESIAN_POINT('',(79.1078754759798,473.010523220612,20.0000000000015));
#5201=CARTESIAN_POINT('',(90.0000000000013,473.010523220612,20.0000000000015));
#5202=CARTESIAN_POINT('',(83.2041524529793,473.010523220612,20.0000000000015));
#5203=CARTESIAN_POINT('',(79.1078754759798,473.010523220612,0.));
#5204=CARTESIAN_POINT('',(79.1078754759798,473.010523220612,0.));
#5205=CARTESIAN_POINT('',(90.0000000000013,473.010523220612,1.47437617670221E-12));
#5206=CARTESIAN_POINT('',(102.451072047422,473.010523220612,1.47437617670221E-12));
#5207=CARTESIAN_POINT('',(90.0000000000013,473.010523220612,10.0000000000007));
#5208=CARTESIAN_POINT('Origin',(79.1078754759798,457.780735240385,0.));
#5209=CARTESIAN_POINT('',(90.0000000000013,457.780735240385,20.0000000000015));
#5210=CARTESIAN_POINT('',(79.1078754759798,457.780735240385,20.0000000000015));
#5211=CARTESIAN_POINT('',(65.3070181435484,457.780735240385,20.0000000000015));
#5212=CARTESIAN_POINT('',(90.0000000000013,457.780735240385,1.47437617670221E-12));
#5213=CARTESIAN_POINT('',(90.0000000000013,457.780735240385,10.0000000000007));
#5214=CARTESIAN_POINT('',(79.1078754759798,457.780735240385,0.));
#5215=CARTESIAN_POINT('',(84.553937737991,457.780735240385,1.47437617670221E-12));
#5216=CARTESIAN_POINT('',(79.1078754759798,457.780735240385,0.));
#5217=CARTESIAN_POINT('Origin',(79.1078754759798,465.395629230499,0.));
#5218=CARTESIAN_POINT('Origin',(79.1078754759798,465.395629230499,20.0000000000015));
#5219=CARTESIAN_POINT('Origin',(79.1078754759798,465.395629230499,1.47437617670221E-12));
#5220=CARTESIAN_POINT('Origin',(90.0000000000013,0.,20.0000000000015));
#5221=CARTESIAN_POINT('',(90.0000000000013,505.5,1.47437617670221E-12));
#5222=CARTESIAN_POINT('',(90.0000000000013,0.,1.47437617670221E-12));
#5223=CARTESIAN_POINT('',(90.0000000000013,505.5,20.0000000000015));
#5224=CARTESIAN_POINT('',(90.0000000000013,505.5,1.47437617670221E-12));
#5225=CARTESIAN_POINT('',(90.0000000000013,0.,20.0000000000015));
#5226=CARTESIAN_POINT('Origin',(90.0000000000013,0.,20.0000000000015));
#5227=CARTESIAN_POINT('',(90.0000000000013,0.,1.47437617670221E-12));
#5228=CARTESIAN_POINT('',(90.0000000000013,0.,20.0000000000015));
#5229=CARTESIAN_POINT('Origin',(90.0000000000013,0.,20.0000000000015));
#5230=CARTESIAN_POINT('',(90.0000000000013,37.,20.0000000000015));
#5231=CARTESIAN_POINT('',(90.0000000000013,0.,20.0000000000015));
#5232=CARTESIAN_POINT('',(90.0000000000013,37.,1.47437617670221E-12));
#5233=CARTESIAN_POINT('',(90.0000000000013,37.,36.2500000000015));
#5234=CARTESIAN_POINT('',(90.0000000000013,0.,1.47437617670221E-12));
#5235=CARTESIAN_POINT('Origin',(90.0000000000013,0.,20.0000000000015));
#5236=CARTESIAN_POINT('',(90.0000000000013,0.,1.47437617670221E-12));
#5237=CARTESIAN_POINT('',(90.0000000000013,0.,20.0000000000015));
#5238=CARTESIAN_POINT('Origin',(90.0000000000013,0.,1.47437617670221E-12));
#5239=CARTESIAN_POINT('',(-89.9999999999987,505.5,1.47437617670221E-12));
#5240=CARTESIAN_POINT('',(45.0000000000012,37.,1.47437617670221E-12));
#5241=CARTESIAN_POINT('Origin',(0.,482.5,62.5000000000015));
#5242=CARTESIAN_POINT('',(-31.5061608111161,482.5,105.000000000001));
#5243=CARTESIAN_POINT('',(31.5061608111161,482.5,105.000000000001));
#5244=CARTESIAN_POINT('',(-89.9999999999987,482.5,105.000000000001));
#5245=CARTESIAN_POINT('',(-31.5061608111161,482.5,20.0000000000015));
#5246=CARTESIAN_POINT('',(-31.5061608111161,482.5,83.7500000000015));
#5247=CARTESIAN_POINT('',(31.5061608111161,482.5,20.0000000000015));
#5248=CARTESIAN_POINT('',(-15.7530804055581,482.5,20.0000000000015));
#5249=CARTESIAN_POINT('',(31.5061608111161,482.5,41.2500000000015));
#5250=CARTESIAN_POINT('Origin',(31.5061608111161,0.,20.0000000000015));
#5251=CARTESIAN_POINT('',(31.5061608111161,60.,20.0000000000015));
#5252=CARTESIAN_POINT('',(31.5061608111161,0.,20.0000000000015));
#5253=CARTESIAN_POINT('',(31.5061608111161,60.,105.000000000001));
#5254=CARTESIAN_POINT('',(31.5061608111161,60.,41.2500000000015));
#5255=CARTESIAN_POINT('',(31.5061608111161,0.,105.000000000001));
#5256=CARTESIAN_POINT('Origin',(-31.5061608111161,0.,20.0000000000015));
#5257=CARTESIAN_POINT('',(-31.5061608111161,60.,20.0000000000015));
#5258=CARTESIAN_POINT('',(-31.5061608111161,0.,20.0000000000015));
#5259=CARTESIAN_POINT('',(-15.7530804055581,60.,20.0000000000015));
#5260=CARTESIAN_POINT('Origin',(-31.5061608111161,0.,105.000000000001));
#5261=CARTESIAN_POINT('',(-31.5061608111161,60.,105.000000000001));
#5262=CARTESIAN_POINT('',(-31.5061608111161,0.,105.000000000001));
#5263=CARTESIAN_POINT('',(-31.5061608111161,60.,83.7500000000015));
#5264=CARTESIAN_POINT('Origin',(0.,60.,62.5000000000015));
#5265=CARTESIAN_POINT('',(-89.9999999999987,60.,105.000000000001));
#5266=CARTESIAN_POINT('Origin',(1.24344978758018E-12,37.,52.5000000000015));
#5267=CARTESIAN_POINT('',(-67.5061608111161,37.,105.000000000001));
#5268=CARTESIAN_POINT('',(67.5061608111161,37.,105.000000000001));
#5269=CARTESIAN_POINT('',(15.7530804055587,37.,105.000000000001));
#5270=CARTESIAN_POINT('',(-67.5061608111161,37.,85.0000000000015));
#5271=CARTESIAN_POINT('',(-67.5061608111161,37.,68.7500000000015));
#5272=CARTESIAN_POINT('',(-51.5061608111161,37.,85.0000000000015));
#5273=CARTESIAN_POINT('',(-25.7530804055574,37.,85.0000000000015));
#5274=CARTESIAN_POINT('',(-51.5061608111161,37.,36.2500000000015));
#5275=CARTESIAN_POINT('',(51.5061608111161,37.,20.0000000000015));
#5276=CARTESIAN_POINT('',(25.7530804055587,37.,20.0000000000015));
#5277=CARTESIAN_POINT('',(51.5061608111161,37.,85.0000000000015));
#5278=CARTESIAN_POINT('',(51.5061608111161,37.,68.7500000000015));
#5279=CARTESIAN_POINT('',(67.5061608111161,37.,85.0000000000015));
#5280=CARTESIAN_POINT('',(33.7530804055587,37.,85.0000000000015));
#5281=CARTESIAN_POINT('',(67.5061608111161,37.,78.7500000000015));
#5282=CARTESIAN_POINT('Origin',(-51.5061608111161,0.,20.0000000000015));
#5283=CARTESIAN_POINT('',(-51.5061608111161,505.5,85.0000000000015));
#5284=CARTESIAN_POINT('',(-51.5061608111161,0.,85.0000000000015));
#5285=CARTESIAN_POINT('',(-51.5061608111161,505.5,1.47437617670221E-12));
#5286=CARTESIAN_POINT('Origin',(-51.5061608111161,0.,85.0000000000015));
#5287=CARTESIAN_POINT('',(-67.5061608111161,505.5,85.0000000000015));
#5288=CARTESIAN_POINT('',(-67.5061608111161,0.,85.0000000000015));
#5289=CARTESIAN_POINT('',(-67.5061608111161,505.5,85.0000000000015));
#5290=CARTESIAN_POINT('Origin',(-67.5061608111161,0.,85.0000000000015));
#5291=CARTESIAN_POINT('',(-67.5061608111161,505.5,105.000000000001));
#5292=CARTESIAN_POINT('',(-67.5061608111161,0.,105.000000000001));
#5293=CARTESIAN_POINT('',(-67.5061608111161,505.5,105.000000000001));
#5294=CARTESIAN_POINT('Origin',(31.5061608111161,0.,105.000000000001));
#5295=CARTESIAN_POINT('',(67.5061608111161,505.5,105.000000000001));
#5296=CARTESIAN_POINT('',(-51.5061608111161,505.5,105.000000000001));
#5297=CARTESIAN_POINT('',(67.5061608111161,0.,105.000000000001));
#5298=CARTESIAN_POINT('Origin',(51.5061608111161,0.,20.0000000000015));
#5299=CARTESIAN_POINT('',(51.5061608111161,505.5,20.0000000000015));
#5300=CARTESIAN_POINT('',(90.0000000000013,505.5,20.0000000000015));
#5301=CARTESIAN_POINT('',(51.5061608111161,0.,20.0000000000015));
#5302=CARTESIAN_POINT('Origin',(51.5061608111161,0.,85.0000000000015));
#5303=CARTESIAN_POINT('',(51.5061608111161,505.5,85.0000000000015));
#5304=CARTESIAN_POINT('',(51.5061608111161,505.5,1.47437617670221E-12));
#5305=CARTESIAN_POINT('',(51.5061608111161,0.,85.0000000000015));
#5306=CARTESIAN_POINT('Origin',(67.5061608111161,0.,85.0000000000015));
#5307=CARTESIAN_POINT('',(67.5061608111161,505.5,85.0000000000015));
#5308=CARTESIAN_POINT('',(67.5061608111161,505.5,85.0000000000015));
#5309=CARTESIAN_POINT('',(67.5061608111161,0.,85.0000000000015));
#5310=CARTESIAN_POINT('Origin',(67.5061608111161,0.,105.000000000001));
#5311=CARTESIAN_POINT('',(67.5061608111161,505.5,105.000000000001));
#5312=CARTESIAN_POINT('Origin',(1.24344978758018E-12,505.5,52.5000000000015));
#6072=UNCERTAINTY_MEASURE_WITH_UNIT(LENGTH_MEASURE(0.01),#6097,
'DISTANCE_ACCURACY_VALUE',
'Maximum model space distance between geometric entities at asserted c
onnectivities');
#6083=UNCERTAINTY_MEASURE_WITH_UNIT(LENGTH_MEASURE(0.01),#6097,
'DISTANCE_ACCURACY_VALUE',
'Maximum model space distance between geometric entities at asserted c
onnectivities');
#6085=(
GEOMETRIC_REPRESENTATION_CONTEXT(3)
GLOBAL_UNCERTAINTY_ASSIGNED_CONTEXT((#6072))
GLOBAL_UNIT_ASSIGNED_CONTEXT((#6097,#6099,#6100))
REPRESENTATION_CONTEXT('','3D')
);
#6096=(
GEOMETRIC_REPRESENTATION_CONTEXT(3)
GLOBAL_UNCERTAINTY_ASSIGNED_CONTEXT((#6083))
GLOBAL_UNIT_ASSIGNED_CONTEXT((#6097,#6099,#6100))
REPRESENTATION_CONTEXT('','3D')
);
#6097=(
LENGTH_UNIT()
NAMED_UNIT(*)
SI_UNIT(.MILLI.,.METRE.)
);
#6099=(
NAMED_UNIT(*)
PLANE_ANGLE_UNIT()
SI_UNIT($,.RADIAN.)
);
#6100=(
NAMED_UNIT(*)
SI_UNIT($,.STERADIAN.)
SOLID_ANGLE_UNIT()
);
#6102=SHAPE_DEFINITION_REPRESENTATION(#6114,#6137);
#6114=PRODUCT_DEFINITION_SHAPE('',$,#6150);
#6137=SHAPE_REPRESENTATION('',(#3727),#6085);
#6148=PRODUCT_DEFINITION_CONTEXT('part definition',#6186,'design');
#6150=PRODUCT_DEFINITION('Base','Base',#6162,#6148);
#6162=PRODUCT_DEFINITION_FORMATION('',$,#6189);
#6186=APPLICATION_CONTEXT(
'Core Data for Automotive Mechanical Design Process');
#6187=PRODUCT_CONTEXT('part definition',#6186,'mechanical');
#6189=PRODUCT('Base','Base',$,(#6187));
#6228=COLOUR_RGB('Dark Blue',0.08,0.2,0.34);
#6229=FILL_AREA_STYLE_COLOUR('',#6228);
#6230=FILL_AREA_STYLE('',(#6229));
#6231=SURFACE_STYLE_FILL_AREA(#6230);
#6232=SURFACE_SIDE_STYLE('',(#6231));
#6233=SURFACE_STYLE_USAGE(.BOTH.,#6232);
#6234=PRESENTATION_STYLE_ASSIGNMENT((#6233));
ENDSEC;
END-ISO-10303-21;
